ISO-10303-21;
HEADER;
FILE_DESCRIPTION (('STEP AP214'),
    '1' );
FILE_NAME ('torque nut 03_iso_ISO 7042-M6-N.step',
    '2026-09-21T15:58:29',
    ( '' ),
    ( '' ),
    'SwSTEP 2.0',
    'SolidWorks 2026',
    '' );
FILE_SCHEMA (( 'AUTOMOTIVE_DESIGN' ));
ENDSEC;

DATA;
#146=FACE_OUTER_BOUND ( 'NONE', #12482, .T. ) ;
#149=PRODUCT_DEFINITION_CONTEXT ( 'detailed design', #18530, 'design' ) ;
#183=LINE ( 'NONE', #25523, #9480 ) ;
#267=CARTESIAN_POINT ( 'NONE',  ( 0.000000000000000000, 0.000000000000000000, -6.000000000000000000 ) ) ;
#307=ORIENTED_EDGE ( 'NONE', *, *, #13420, .T. ) ;
#319=CARTESIAN_POINT ( 'NONE',  ( -4.749999999999999112, 0.000000000000000000, 0.000000000000000000 ) ) ;
#322=CARTESIAN_POINT ( 'NONE',  ( 0.000000000000000000, 0.000000000000000000, -6.000000000000000000 ) ) ;
#400=CARTESIAN_POINT ( 'NONE',  ( 0.000000000000000000, 0.000000000000000000, -0.3851141460153411078 ) ) ;
#420=FACE_OUTER_BOUND ( 'NONE', #10081, .T. ) ;
#430=CARTESIAN_POINT ( 'NONE',  ( 3.000000000000000000, 0.000000000000000000, -25.03750572909317285 ) ) ;
#486=EDGE_CURVE ( 'NONE', #21666, #32300, #22317, .T. ) ;
#566=ADVANCED_FACE ( 'NONE', ( #36328 ), #1621, .T. ) ;
#574=EDGE_LOOP ( 'NONE', ( #29728, #17619, #5808 ) ) ;
#580=CARTESIAN_POINT ( 'NONE',  ( -4.999999999999999112, 2.691270400161067666, -1.881368198414903548 ) ) ;
#588=VECTOR ( 'NONE', #15784, 1000.000000000000000 ) ;
#593=CARTESIAN_POINT ( 'NONE',  ( 0.000000000000000000, 0.000000000000000000, -6.000000000000000000 ) ) ;
#600=EDGE_CURVE ( 'NONE', #15155, #20425, #19004, .T. ) ;
#614=FILL_AREA_STYLE ('',( #23664 ) ) ;
#657=CARTESIAN_POINT ( 'NONE',  ( 2.500000000000000000, 0.000000000000000000, -5.624496230895140947 ) ) ;
#727=EDGE_CURVE ( 'NONE', #10440, #26731, #22992, .T. ) ;
#754=CARTESIAN_POINT ( 'NONE',  ( -4.999999999999999112, 1.831554690317574341, -1.158389257021580576 ) ) ;
#816=VERTEX_POINT ( 'NONE', #31784 ) ;
#854=AXIS2_PLACEMENT_3D ( 'NONE', #593, #17839, #15403 ) ;
#1107=CARTESIAN_POINT ( 'NONE',  ( 4.180704885107411783, 3.359771601077109260, -5.801655677627843843 ) ) ;
#1126=CARTESIAN_POINT ( 'NONE',  ( 5.000000000000000888, -2.886751345948134873, -2.080000000000000071 ) ) ;
#1166=CARTESIAN_POINT ( 'NONE',  ( 0.000000000000000000, 0.000000000000000000, -6.000000000000000000 ) ) ;
#1204=CARTESIAN_POINT ( 'NONE',  ( 3.000000000000000000, 0.000000000000000000, -6.000000000000001776 ) ) ;
#1217=EDGE_CURVE ( 'NONE', #24448, #33082, #4139, .T. ) ;
#1389=CARTESIAN_POINT ( 'NONE',  ( 5.000000000000000000, 2.059541880722000506, -1.329159518034687126 ) ) ;
#1440=CARTESIAN_POINT ( 'NONE',  ( 0.000000000000000000, 0.000000000000000000, -6.000000000000000000 ) ) ;
#1459=SURFACE_SIDE_STYLE ('',( #35797 ) ) ;
#1522=CONICAL_SURFACE ( 'NONE', #30306, 5.000000000000000888, 1.047197551196596299 ) ;
#1546=EDGE_LOOP ( 'NONE', ( #8388, #6636, #36440, #37077, #4577 ) ) ;
#1601=CONICAL_SURFACE ( 'NONE', #6387, 2.449999999999998845, 0.9599310885968813656 ) ;
#1614=DIRECTION ( 'NONE',  ( -0.000000000000000000, -0.000000000000000000, 1.000000000000000000 ) ) ;
#1621=CONICAL_SURFACE ( 'NONE', #14196, 5.000000000000000888, 1.047197551196596299 ) ;
#1679=CARTESIAN_POINT ( 'NONE',  ( -5.000000000000000000, -0.5603747650654237189, -0.5678343202077608121 ) ) ;
#1703=CARTESIAN_POINT ( 'NONE',  ( 5.000000000000000000, 6.074766241781102566E-16, -0.5080592402122449114 ) ) ;
#1801=FACE_OUTER_BOUND ( 'NONE', #32971, .T. ) ;
#1803=EDGE_CURVE ( 'NONE', #32300, #36720, #36181, .T. ) ;
#1805=CARTESIAN_POINT ( 'NONE',  ( 5.000000000000000888, 0.000000000000000000, -6.000000000000000000 ) ) ;
#1811=AXIS2_PLACEMENT_3D ( 'NONE', #3822, #16162, #6468 ) ;
#1840=EDGE_CURVE ( 'NONE', #10511, #28959, #19203, .T. ) ;
#1868=CARTESIAN_POINT ( 'NONE',  ( -2.449999999999998845, 3.000384657911014384E-16, -0.3851141460153411078 ) ) ;
#1883=CARTESIAN_POINT ( 'NONE',  ( 5.000000000000000000, -1.096207231254244352, -0.7463930790433302986 ) ) ;
#1890=ADVANCED_FACE ( 'NONE', ( #17026, #2040 ), #27915, .T. ) ;
#1916=CARTESIAN_POINT ( 'NONE',  ( -5.000000000000000000, 2.886751345948126879, -6.000000000000000000 ) ) ;
#1957=CARTESIAN_POINT ( 'NONE',  ( 0.000000000000000000, 0.000000000000000000, -6.000000000000000000 ) ) ;
#1974=CARTESIAN_POINT ( 'NONE',  ( 0.000000000000000000, 0.000000000000000000, 0.000000000000000000 ) ) ;
#1983=DIRECTION ( 'NONE',  ( 0.8191520442889890230, 1.003171929053521295E-16, -0.5735764363510501562 ) ) ;
#1997=CARTESIAN_POINT ( 'NONE',  ( -1.552113441248129000, 4.877389578778817736, -0.7348938709837885552 ) ) ;
#2040=FACE_OUTER_BOUND ( 'NONE', #9470, .T. ) ;
#2086=AXIS2_PLACEMENT_3D ( 'NONE', #11199, #10843, #19459 ) ;
#2091=EDGE_CURVE ( 'NONE', #33082, #32864, #33294, .T. ) ;
#2189=PRODUCT_DEFINITION_FORMATION_WITH_SPECIFIED_SOURCE ( 'ANY', '', #36694, .NOT_KNOWN. ) ;
#2190=DIRECTION ( 'NONE',  ( -0.000000000000000000, -0.000000000000000000, 1.000000000000000000 ) ) ;
#2246=CARTESIAN_POINT ( 'NONE',  ( -5.000000000000000000, -2.886751345948137981, -5.553418012614792509 ) ) ;
#2298=AXIS2_PLACEMENT_3D ( 'NONE', #15101, #9838, #6839 ) ;
#2323=EDGE_CURVE ( 'NONE', #17546, #20171, #32198, .T. ) ;
#2420=VERTEX_POINT ( 'NONE', #11720 ) ;
#2519=ORIENTED_EDGE ( 'NONE', *, *, #13420, .F. ) ;
#2522=DIRECTION ( 'NONE',  ( 0.000000000000000000, -0.000000000000000000, 1.000000000000000000 ) ) ;
#2526=ORIENTED_EDGE ( 'NONE', *, *, #7869, .F. ) ;
#2530=ORIENTED_EDGE ( 'NONE', *, *, #11336, .T. ) ;
#2539=EDGE_CURVE ( 'NONE', #2420, #9972, #9101, .T. ) ;
#2562=CARTESIAN_POINT ( 'NONE',  ( -3.453178355211937944, 3.779809238954856099, -0.7375898304884446199 ) ) ;
#2607=ADVANCED_FACE ( 'NONE', ( #21276 ), #15464, .T. ) ;
#2684=EDGE_CURVE ( 'NONE', #4982, #10511, #23245, .T. ) ;
#2740=EDGE_LOOP ( 'NONE', ( #28222, #6960, #21599 ) ) ;
#2813=CARTESIAN_POINT ( 'NONE',  ( -9.974659986866640793E-15, -5.773502691896262640, -5.553418012614792509 ) ) ;
#2924=DIRECTION ( 'NONE',  ( -1.000000000000000000, 0.000000000000000000, 0.000000000000000000 ) ) ;
#2930=EDGE_CURVE ( 'NONE', #34239, #16670, #26318, .T. ) ;
#2976=B_SPLINE_CURVE_WITH_KNOTS ( 'NONE', 3,
 ( #7325, #30922, #7886, #25147, #13310, #33388, #27384, #1883, #8056, #18951, #24757, #13864, #30737, #1703 ),
 .UNSPECIFIED., .F., .F.,
 ( 4, 2, 2, 2, 2, 2, 4 ),
 ( 0.01481111731982464805, 0.01564725794959783214, 0.01648339857937101624, 0.01690146889425760829, 0.01731953920914420034, 0.01773760952403079239, 0.01815567983891738443 ),
 .UNSPECIFIED. ) ;
#2987=EDGE_CURVE ( 'NONE', #9972, #36720, #13959, .T. ) ;
#3029=DIRECTION ( 'NONE',  ( 1.000000000000000000, 0.000000000000000000, 0.000000000000000000 ) ) ;
#3176=AXIS2_PLACEMENT_3D ( 'NONE', #35134, #12208, #24227 ) ;
#3453=ORIENTED_EDGE ( 'NONE', *, *, #6651, .T. ) ;
#3462=CARTESIAN_POINT ( 'NONE',  ( 0.1714266706912579152, -5.674529457426388923, -1.878862934774795823 ) ) ;
#3729=FACE_OUTER_BOUND ( 'NONE', #11059, .T. ) ;
#3757=ORIENTED_EDGE ( 'NONE', *, *, #13202, .F. ) ;
#3780=B_SPLINE_CURVE_WITH_KNOTS ( 'NONE', 3,
 ( #15796, #23677, #26875, #35135, #12605, #20871, #24059, #15230, #18992, #24993, #13903, #16185, #36431, #18800, #24627, #30218, #19352, #33787, #16544, #10738 ),
 .UNSPECIFIED., .F., .F.,
 ( 4, 2, 2, 2, 2, 2, 2, 2, 2, 4 ),
 ( 2.781148923622390442E-07, 0.0008372784139766601373, 0.001674278713060957900, 0.002511279012145256097, 0.003348279311229553860, 0.003766779460771703825, 0.004185279610313853357, 0.005022279909398152421, 0.005859280208482451485, 0.006696280507566749682 ),
 .UNSPECIFIED. ) ;
#3781=SURFACE_SIDE_STYLE ('',( #11655 ) ) ;
#3822=CARTESIAN_POINT ( 'NONE',  ( -2.503857664561936813E-16, -5.773502691896267081, -6.000000000000000000 ) ) ;
#3861=EDGE_CURVE ( 'NONE', #29787, #9742, #30985, .T. ) ;
#3952=VECTOR ( 'NONE', #30376, 999.9999999999998863 ) ;
#3961=CARTESIAN_POINT ( 'NONE',  ( 3.447886558751866115, 3.782864459065575780, -0.7348938709837807837 ) ) ;
#3975=LINE ( 'NONE', #12960, #588 ) ;
#3988=ORIENTED_EDGE ( 'NONE', *, *, #22035, .T. ) ;
#4059=EDGE_LOOP ( 'NONE', ( #3988, #26248, #5156, #26968, #33262 ) ) ;
#4069=ORIENTED_EDGE ( 'NONE', *, *, #29825, .T. ) ;
#4139=B_SPLINE_CURVE_WITH_KNOTS ( 'NONE', 3,
 ( #14370, #14723, #26166, #25813 ),
 .UNSPECIFIED., .F., .F.,
 ( 4, 4 ),
 ( 2.380735200821679637E-07, 0.002921158011986721599 ),
 .UNSPECIFIED. ) ;
#4149=AXIS2_PLACEMENT_3D ( 'NONE', #9549, #23990, #4472 ) ;
#4160=CARTESIAN_POINT ( 'NONE',  ( 4.651285141665000289, 3.088081963278261011, -1.686035282245264444 ) ) ;
#4198=CIRCLE ( 'NONE', #6592, 5.000000000000000888 ) ;
#4291=( LENGTH_UNIT ( ) NAMED_UNIT ( * ) SI_UNIT ( .MILLI., .METRE. ) );
#4369=ORIENTED_EDGE ( 'NONE', *, *, #6651, .F. ) ;
#4401=CARTESIAN_POINT ( 'NONE',  ( -5.000000000000000000, 0.000000000000000000, -6.000000000000000000 ) ) ;
#4449=DIRECTION ( 'NONE',  ( 0.000000000000000000, -0.000000000000000000, 1.000000000000000000 ) ) ;
#4472=DIRECTION ( 'NONE',  ( 1.000000000000000000, 0.000000000000000000, 0.000000000000000000 ) ) ;
#4494=FACE_OUTER_BOUND ( 'NONE', #21338, .T. ) ;
#4577=ORIENTED_EDGE ( 'NONE', *, *, #14913, .F. ) ;
#4603=DIRECTION ( 'NONE',  ( -1.000000000000000000, 0.000000000000000000, 0.000000000000000000 ) ) ;
#4655=EDGE_CURVE ( 'NONE', #35263, #28959, #33712, .T. ) ;
#4681=CARTESIAN_POINT ( 'NONE',  ( -3.556264818047238485, -3.720292241887096285, -5.918341802876226687 ) ) ;
#4708=UNCERTAINTY_MEASURE_WITH_UNIT (LENGTH_MEASURE( 1.000000000000000082E-05 ), #33345, 'distance_accuracy_value', 'NONE');
#4737=CARTESIAN_POINT ( 'NONE',  ( 6.078523336270777024E-16, 5.773502691896261751, -6.000000000000000000 ) ) ;
#4747=DIRECTION ( 'NONE',  ( 0.000000000000000000, 0.000000000000000000, 1.000000000000000000 ) ) ;
#4856=EDGE_CURVE ( 'NONE', #35263, #10511, #22100, .T. ) ;
#4924=EDGE_CURVE ( 'NONE', #15155, #13152, #13308, .T. ) ;
#4982=VERTEX_POINT ( 'NONE', #18760 ) ;
#5001=CARTESIAN_POINT ( 'NONE',  ( -0.9154378789997292820, 5.244974386029388036, -1.156968425231163167 ) ) ;
#5020=FACE_OUTER_BOUND ( 'NONE', #23353, .T. ) ;
#5099=APPLICATION_CONTEXT ( 'automotive_design' ) ;
#5122=B_SPLINE_CURVE_WITH_KNOTS ( 'NONE', 3,
 ( #15384, #20821, #9382, #21011, #15192, #754, #23456, #30004, #580, #15020 ),
 .UNSPECIFIED., .F., .F.,
 ( 4, 2, 2, 2, 4 ),
 ( 0.01815567983891738443, 0.01899359644517026671, 0.01983151305142314552, 0.02066942965767602780, 0.02150734626392890661 ),
 .UNSPECIFIED. ) ;
#5156=ORIENTED_EDGE ( 'NONE', *, *, #727, .F. ) ;
#5184=ORIENTED_EDGE ( 'NONE', *, *, #29825, .F. ) ;
#5214=AXIS2_PLACEMENT_3D ( 'NONE', #32848, #15966, #13153 ) ;
#5271=CIRCLE ( 'NONE', #11220, 2.500000000000000000 ) ;
#5431=DIRECTION ( 'NONE',  ( -1.000000000000000000, 0.000000000000000000, 0.000000000000000000 ) ) ;
#5474=ADVANCED_FACE ( 'NONE', ( #5666 ), #1601, .F. ) ;
#5508=VECTOR ( 'NONE', #33063, 1000.000000000000000 ) ;
#5522=ORIENTED_EDGE ( 'NONE', *, *, #28428, .F. ) ;
#5601=AXIS2_PLACEMENT_3D ( 'NONE', #36815, #14116, #23312 ) ;
#5666=FACE_OUTER_BOUND ( 'NONE', #32992, .T. ) ;
#5682=B_SPLINE_CURVE_WITH_KNOTS ( 'NONE', 3,
 ( #21895, #16649, #33341, #7281 ),
 .UNSPECIFIED., .F., .F.,
 ( 4, 4 ),
 ( 2.380735200870747991E-07, 0.002921158011986710323 ),
 .UNSPECIFIED. ) ;
#5720=CIRCLE ( 'NONE', #24263, 4.749999999999999112 ) ;
#5808=ORIENTED_EDGE ( 'NONE', *, *, #25444, .T. ) ;
#5831=CONICAL_SURFACE ( 'NONE', #5214, 2.449999999999998845, 0.9599310885968813656 ) ;
#5863=DIRECTION ( 'NONE',  ( 0.5000000000000009992, 0.8660254037844381525, -0.000000000000000000 ) ) ;
#5935=CARTESIAN_POINT ( 'NONE',  ( 0.000000000000000000, 0.000000000000000000, -5.624496230895140947 ) ) ;
#5974=ORIENTED_EDGE ( 'NONE', *, *, #22035, .F. ) ;
#5979=FACE_OUTER_BOUND ( 'NONE', #28305, .T. ) ;
#5990=DIRECTION ( 'NONE',  ( 1.000000000000000000, 0.000000000000000000, 0.000000000000000000 ) ) ;
#6025=AXIS2_PLACEMENT_3D ( 'NONE', #28458, #22125, #5431 ) ;
#6057=CARTESIAN_POINT ( 'NONE',  ( 5.000000000000000888, 0.000000000000000000, -6.000000000000000000 ) ) ;
#6083=CARTESIAN_POINT ( 'NONE',  ( 2.018853055115724882, -4.607917337070903230, -0.5666985376598668855 ) ) ;
#6112=EDGE_CURVE ( 'NONE', #27114, #21710, #12853, .T. ) ;
#6256=CARTESIAN_POINT ( 'NONE',  ( 0.3487148583350060949, -5.572172074566128508, -1.686035282245279765 ) ) ;
#6268=DIRECTION ( 'NONE',  ( 1.000000000000000000, 0.000000000000000000, 0.000000000000000000 ) ) ;
#6288=CARTESIAN_POINT ( 'NONE',  ( 2.449999999999998845, 0.000000000000000000, -0.3851141460153411078 ) ) ;
#6304=SHAPE_DEFINITION_REPRESENTATION ( #16936, #35440 ) ;
#6343=CARTESIAN_POINT ( 'NONE',  ( 0.8192951148925871063, -5.300482436767286920, -5.801655677627835850 ) ) ;
#6380=CARTESIAN_POINT ( 'NONE',  ( 0.000000000000000000, 0.000000000000000000, -25.03750572909317285 ) ) ;
#6387=AXIS2_PLACEMENT_3D ( 'NONE', #400, #14480, #11474 ) ;
#6414=PLANE ( 'NONE',  #18701 ) ;
#6426=DIRECTION ( 'NONE',  ( 0.000000000000000000, -0.000000000000000000, 1.000000000000000000 ) ) ;
#6429=ORIENTED_EDGE ( 'NONE', *, *, #27251, .T. ) ;
#6468=DIRECTION ( 'NONE',  ( 0.8660254037844382635, 0.5000000000000005551, 0.000000000000000000 ) ) ;
#6476=CARTESIAN_POINT ( 'NONE',  ( -5.000000000000000000, 2.886751345948126879, -2.079999999999992077 ) ) ;
#6558=ORIENTED_EDGE ( 'NONE', *, *, #486, .F. ) ;
#6592=AXIS2_PLACEMENT_3D ( 'NONE', #1166, #9605, #24038 ) ;
#6606=VECTOR ( 'NONE', #13294, 1000.000000000000227 ) ;
#6636=ORIENTED_EDGE ( 'NONE', *, *, #2323, .T. ) ;
#6651=EDGE_CURVE ( 'NONE', #29787, #4982, #4198, .T. ) ;
#6660=CARTESIAN_POINT ( 'NONE',  ( 0.000000000000000000, 0.000000000000000000, -6.000000000000001776 ) ) ;
#6676=ORIENTED_EDGE ( 'NONE', *, *, #20106, .F. ) ;
#6747=DIRECTION ( 'NONE',  ( 1.000000000000000000, 0.000000000000000000, 0.000000000000000000 ) ) ;
#6788=LINE ( 'NONE', #430, #11150 ) ;
#6809=ORIENTED_EDGE ( 'NONE', *, *, #8541, .F. ) ;
#6837=ORIENTED_EDGE ( 'NONE', *, *, #2091, .T. ) ;
#6839=DIRECTION ( 'NONE',  ( 1.000000000000000000, 0.000000000000000000, 0.000000000000000000 ) ) ;
#6864=CARTESIAN_POINT ( 'NONE',  ( 5.000000000000000000, 2.886751345948134428, -2.080000000000000071 ) ) ;
#6902=CARTESIAN_POINT ( 'NONE',  ( 2.500000000000003109, -4.330127018922192761, -6.000000000000000000 ) ) ;
#6903=ORIENTED_EDGE ( 'NONE', *, *, #29976, .F. ) ;
#6935=DIRECTION ( 'NONE',  ( -1.000000000000000000, 0.000000000000000000, 0.000000000000000000 ) ) ;
#6960=ORIENTED_EDGE ( 'NONE', *, *, #15972, .T. ) ;
#6967=FACE_BOUND ( 'NONE', #12128, .T. ) ;
#7061=DIRECTION ( 'NONE',  ( 1.000000000000000000, 0.000000000000000000, 0.000000000000000000 ) ) ;
#7110=DIRECTION ( 'NONE',  ( 1.000000000000000000, 0.000000000000000000, 0.000000000000000000 ) ) ;
#7137=CARTESIAN_POINT ( 'NONE',  ( -0.8179331680533066251, -5.301268757141566645, -5.826062401966622062 ) ) ;
#7160=CARTESIAN_POINT ( 'NONE',  ( 2.618768541235299896, 4.261555969668734178, -0.5078976954042870862 ) ) ;
#7164=B_SPLINE_CURVE_WITH_KNOTS ( 'NONE', 3,
 ( #21757, #33192, #27585, #7513, #13318, #10161, #18963, #15769, #7334, #7160, #21398, #9765, #18199, #3961, #21199, #32841, #18599, #4160, #15404, #24405 ),
 .UNSPECIFIED., .F., .F.,
 ( 4, 2, 2, 2, 2, 2, 2, 2, 2, 4 ),
 ( 2.781148923614798380E-07, 0.0008372784139766645825, 0.001674278713060967658, 0.002511279012145270842, 0.003348279311229572942, 0.003766779460771723775, 0.004185279610313873307, 0.005022279909398174105, 0.005859280208482472302, 0.006696280507566771366 ),
 .UNSPECIFIED. ) ;
#7249=CARTESIAN_POINT ( 'NONE',  ( -2.500000000000000000, 3.061616997868383141E-16, -5.624496230895140947 ) ) ;
#7255=CARTESIAN_POINT ( 'NONE',  ( 3.000000000000000000, 3.673940397442059868E-16, -5.974599999999999689 ) ) ;
#7281=CARTESIAN_POINT ( 'NONE',  ( -2.500000000000003997, 4.330127018922192761, -6.000000000000000000 ) ) ;
#7285=ORIENTED_EDGE ( 'NONE', *, *, #2323, .F. ) ;
#7311=CARTESIAN_POINT ( 'NONE',  ( 0.000000000000000000, 0.000000000000000000, 0.000000000000000000 ) ) ;
#7325=CARTESIAN_POINT ( 'NONE',  ( 5.000000000000000888, -2.886751345948134873, -2.080000000000000071 ) ) ;
#7334=CARTESIAN_POINT ( 'NONE',  ( 2.255011273957053586, 4.471571325851512846, -0.5083873451168745561 ) ) ;
#7340=ORIENTED_EDGE ( 'NONE', *, *, #2987, .F. ) ;
#7362=ORIENTED_EDGE ( 'NONE', *, *, #28372, .T. ) ;
#7409=ORIENTED_EDGE ( 'NONE', *, *, #4856, .T. ) ;
#7513=CARTESIAN_POINT ( 'NONE',  ( 0.7178748134486927501, 5.359037475107204962, -1.327869168827484403 ) ) ;
#7568=ORIENTED_EDGE ( 'NONE', *, *, #13202, .T. ) ;
#7583=CARTESIAN_POINT ( 'NONE',  ( -2.500000000000003997, 4.330127018922192761, -6.000000000000000000 ) ) ;
#7625=CARTESIAN_POINT ( 'NONE',  ( -5.000000000000000000, 2.886751345948126879, -6.000000000000000000 ) ) ;
#7640=CARTESIAN_POINT ( 'NONE',  ( -2.260257450329326456, 4.468542444510766209, -0.5197061503823194872 ) ) ;
#7660=FILL_AREA_STYLE ('',( #30335 ) ) ;
#7743=MANIFOLD_SOLID_BREP ( 'EndChamfer', #18386 ) ;
#7799=CARTESIAN_POINT ( 'NONE',  ( -1.653121499799246497, 4.819072548984005167, -5.948595712916174172 ) ) ;
#7810=LINE ( 'NONE', #13804, #20624 ) ;
#7866=CARTESIAN_POINT ( 'NONE',  ( -5.000000000000000888, -2.488288133785819589, -1.689848211693934621 ) ) ;
#7869=EDGE_CURVE ( 'NONE', #32183, #23730, #3975, .T. ) ;
#7886=CARTESIAN_POINT ( 'NONE',  ( 5.000000000000000888, -2.488288133785820033, -1.689848211693934621 ) ) ;
#7964=ORIENTED_EDGE ( 'NONE', *, *, #18555, .T. ) ;
#7999=CARTESIAN_POINT ( 'NONE',  ( -4.652319770550016109, 3.087484620012986625, -1.687189089856314217 ) ) ;
#8002=EDGE_CURVE ( 'NONE', #24448, #20171, #36965, .T. ) ;
#8012=CONICAL_SURFACE ( 'NONE', #28368, 4.749999999999999112, 0.4572823821333981131 ) ;
#8056=CARTESIAN_POINT ( 'NONE',  ( 5.000000000000000000, -0.9645339558193165574, -0.6919071587033235327 ) ) ;
#8114=EDGE_LOOP ( 'NONE', ( #36553, #21356, #12693, #23015 ) ) ;
#8388=ORIENTED_EDGE ( 'NONE', *, *, #22864, .T. ) ;
#8473=CARTESIAN_POINT ( 'NONE',  ( 0.000000000000000000, 0.000000000000000000, -6.000000000000000000 ) ) ;
#8541=EDGE_CURVE ( 'NONE', #20425, #816, #26212, .T. ) ;
#8608=ORIENTED_EDGE ( 'NONE', *, *, #11336, .F. ) ;
#8675=SURFACE_STYLE_USAGE ( .BOTH. , #3781 ) ;
#8700=CONICAL_SURFACE ( 'NONE', #2086, 5.000000000000000888, 1.047197551196596299 ) ;
#8822=CARTESIAN_POINT ( 'NONE',  ( 0.000000000000000000, 0.000000000000000000, 0.000000000000000000 ) ) ;
#8846=CARTESIAN_POINT ( 'NONE',  ( 5.000000000000000000, 2.886751345948125991, -6.000000000000000000 ) ) ;
#8896=CARTESIAN_POINT ( 'NONE',  ( 0.000000000000000000, 0.000000000000000000, 0.000000000000000000 ) ) ;
#8897=CARTESIAN_POINT ( 'NONE',  ( 3.453178355211938388, -3.779809238954861428, -0.7375898304884541679 ) ) ;
#8919=ORIENTED_EDGE ( 'NONE', *, *, #14680, .F. ) ;
#8958=ADVANCED_FACE ( 'NONE', ( #34897 ), #1522, .T. ) ;
#9033=ORIENTED_EDGE ( 'NONE', *, *, #30558, .T. ) ;
#9065=PRODUCT_DEFINITION ( 'UNKNOWN', '', #2189, #149 ) ;
#9080=FACE_OUTER_BOUND ( 'NONE', #25614, .T. ) ;
#9101=LINE ( 'NONE', #6288, #23220 ) ;
#9153=CARTESIAN_POINT ( 'NONE',  ( 2.925285743277526329, 4.084588180558403891, -5.989444439476610427 ) ) ;
#9194=CARTESIAN_POINT ( 'NONE',  ( 5.000000000000002665, -2.886751345948134873, -5.553418012614792509 ) ) ;
#9281=B_SPLINE_CURVE_WITH_KNOTS ( 'NONE', 3,
 ( #31092, #30344, #22658, #30889, #4681, #11206, #27543, #16664 ),
 .UNSPECIFIED., .F., .F.,
 ( 4, 2, 2, 4 ),
 ( 0.002921158011986722466, 0.003648658599403074854, 0.004376159186819426374, 0.005831160361652130281 ),
 .UNSPECIFIED. ) ;
#9331=CARTESIAN_POINT ( 'NONE',  ( 0.000000000000000000, 0.000000000000000000, -6.000000000000000000 ) ) ;
#9382=CARTESIAN_POINT ( 'NONE',  ( -4.999999999999999112, 0.5616961504262225624, -0.5576671450146215570 ) ) ;
#9456=CARTESIAN_POINT ( 'NONE',  ( 3.675296855064185575, -3.651569063273171434, -0.8655517945778166133 ) ) ;
#9470=EDGE_LOOP ( 'NONE', ( #4369, #11788, #31532, #32674, #15160, #16126 ) ) ;
#9480=VECTOR ( 'NONE', #14276, 999.9999999999998863 ) ;
#9486=DIRECTION ( 'NONE',  ( -1.000000000000000000, 0.000000000000000000, 0.000000000000000000 ) ) ;
#9494=CARTESIAN_POINT ( 'NONE',  ( -5.000000000000000888, 0.9828435001097632906, -5.956909652965543422 ) ) ;
#9527=DIRECTION ( 'NONE',  ( -1.000000000000000000, -1.776356839400250465E-15, 0.000000000000000000 ) ) ;
#9549=CARTESIAN_POINT ( 'NONE',  ( 0.000000000000000000, 0.000000000000000000, -25.03750572909317285 ) ) ;
#9605=DIRECTION ( 'NONE',  ( 0.000000000000000000, -0.000000000000000000, 1.000000000000000000 ) ) ;
#9674=CARTESIAN_POINT ( 'NONE',  ( -5.000000000000000000, 2.886751345948137981, -5.553418012614792509 ) ) ;
#9742=VERTEX_POINT ( 'NONE', #25543 ) ;
#9765=CARTESIAN_POINT ( 'NONE',  ( 2.981146944884248473, 4.052336700773506273, -0.5666985376598466795 ) ) ;
#9838=DIRECTION ( 'NONE',  ( -0.000000000000000000, -0.000000000000000000, 1.000000000000000000 ) ) ;
#9841=CARTESIAN_POINT ( 'NONE',  ( -5.000000000000000000, 2.419979747126332903, -5.688163366729713566 ) ) ;
#9918=CARTESIAN_POINT ( 'NONE',  ( -5.000000000000000000, -0.6964580643377609181, -0.6026403643956899092 ) ) ;
#9972=VERTEX_POINT ( 'NONE', #20451 ) ;
#9984=CARTESIAN_POINT ( 'NONE',  ( 5.000000000000000000, 6.074766241781102566E-16, -0.5080592402122449114 ) ) ;
#10029=PLANE ( 'NONE',  #31481 ) ;
#10081=EDGE_LOOP ( 'NONE', ( #10189, #7568, #2526, #34230, #24074 ) ) ;
#10107=ORIENTED_EDGE ( 'NONE', *, *, #14913, .T. ) ;
#10109=PRESENTATION_STYLE_ASSIGNMENT (( #19285 ) ) ;
#10120=ORIENTED_EDGE ( 'NONE', *, *, #32709, .T. ) ;
#10161=CARTESIAN_POINT ( 'NONE',  ( 1.324703144935786447, 5.008684974571240289, -0.8655517945778323785 ) ) ;
#10189=ORIENTED_EDGE ( 'NONE', *, *, #727, .T. ) ;
#10230=CARTESIAN_POINT ( 'NONE',  ( 0.000000000000000000, 0.000000000000000000, -5.974599999999999689 ) ) ;
#10333=EDGE_CURVE ( 'NONE', #10511, #10440, #17041, .T. ) ;
#10389=AXIS2_PLACEMENT_3D ( 'NONE', #17301, #11635, #30287 ) ;
#10440=VERTEX_POINT ( 'NONE', #26784 ) ;
#10476=CARTESIAN_POINT ( 'NONE',  ( -5.000000000000000000, -1.096207231254244352, -0.7463930790433302986 ) ) ;
#10511=VERTEX_POINT ( 'NONE', #6902 ) ;
#10581=CARTESIAN_POINT ( 'NONE',  ( -5.000000000000000000, -0.9724665692850904541, -5.958069561147902427 ) ) ;
#10605=CARTESIAN_POINT ( 'NONE',  ( 1.301042606982605321E-15, 5.773502691896264416, -5.553418012614792509 ) ) ;
#10637=CARTESIAN_POINT ( 'NONE',  ( -4.088737910769898676, 3.412868758467427988, -1.160540885688320589 ) ) ;
#10695=UNCERTAINTY_MEASURE_WITH_UNIT (LENGTH_MEASURE( 1.000000000000000082E-05 ), #4291, 'distance_accuracy_value', 'NONE');
#10738=CARTESIAN_POINT ( 'NONE',  ( -5.000000000000000000, -2.886751345948134428, -2.080000000000000071 ) ) ;
#10769=ADVANCED_FACE ( 'NONE', ( #23697 ), #35149, .T. ) ;
#10825=CARTESIAN_POINT ( 'NONE',  ( -5.000000000000000000, 2.886751345948126879, -2.079999999999992077 ) ) ;
#10843=DIRECTION ( 'NONE',  ( -0.000000000000000000, -0.000000000000000000, 1.000000000000000000 ) ) ;
#10986=DIRECTION ( 'NONE',  ( 0.000000000000000000, 0.000000000000000000, 1.000000000000000000 ) ) ;
#11059=EDGE_LOOP ( 'NONE', ( #5184, #30125, #21252, #24634 ) ) ;
#11072=DIRECTION ( 'NONE',  ( 0.000000000000000000, 0.000000000000000000, 1.000000000000000000 ) ) ;
#11131=DIRECTION ( 'NONE',  ( -0.000000000000000000, -0.000000000000000000, 1.000000000000000000 ) ) ;
#11150=VECTOR ( 'NONE', #11866, 1000.000000000000000 ) ;
#11177=CARTESIAN_POINT ( 'NONE',  ( -2.744988726042923766, 4.188682711992889551, -0.5083873451168725577 ) ) ;
#11199=CARTESIAN_POINT ( 'NONE',  ( 0.000000000000000000, 0.000000000000000000, -6.000000000000000000 ) ) ;
#11206=CARTESIAN_POINT ( 'NONE',  ( -4.180704885107413560, -3.359771601077115921, -5.801655677627839403 ) ) ;
#11220=AXIS2_PLACEMENT_3D ( 'NONE', #16438, #22947, #34769 ) ;
#11336=EDGE_CURVE ( 'NONE', #20171, #12255, #7164, .T. ) ;
#11419=ORIENTED_EDGE ( 'NONE', *, *, #6112, .F. ) ;
#11474=DIRECTION ( 'NONE',  ( 1.000000000000000000, 0.000000000000000000, 0.000000000000000000 ) ) ;
#11518=CARTESIAN_POINT ( 'NONE',  ( 3.035766082959412415E-15, 5.773502691896260863, -2.080000000000000071 ) ) ;
#11522=EDGE_LOOP ( 'NONE', ( #21753, #13687, #6837 ) ) ;
#11566=DIRECTION ( 'NONE',  ( -0.4415113423096792000, 0.000000000000000000, -0.8972556684757725387 ) ) ;
#11635=DIRECTION ( 'NONE',  ( -0.000000000000000000, -0.000000000000000000, 1.000000000000000000 ) ) ;
#11655=SURFACE_STYLE_FILL_AREA ( #614 ) ;
#11720=CARTESIAN_POINT ( 'NONE',  ( 2.500000000000000000, 0.000000000000000000, -0.3501037691048548561 ) ) ;
#11788=ORIENTED_EDGE ( 'NONE', *, *, #27251, .F. ) ;
#11798=EDGE_CURVE ( 'NONE', #2420, #32300, #11912, .T. ) ;
#11813=FACE_OUTER_BOUND ( 'NONE', #29658, .T. ) ;
#11866=DIRECTION ( 'NONE',  ( -0.000000000000000000, -0.000000000000000000, 1.000000000000000000 ) ) ;
#11881=CARTESIAN_POINT ( 'NONE',  ( 2.260257450329328233, -4.468542444510769762, -0.5197061503823295903 ) ) ;
#11912=CIRCLE ( 'NONE', #37067, 2.500000000000000000 ) ;
#12003=CARTESIAN_POINT ( 'NONE',  ( 5.000000000000000000, -0.4878135028931873673, -6.000000000000001776 ) ) ;
#12072=DIRECTION ( 'NONE',  ( -0.000000000000000000, -0.000000000000000000, 1.000000000000000000 ) ) ;
#12119=CARTESIAN_POINT ( 'NONE',  ( -2.500000000000000000, 3.061616997868383141E-16, -0.3501037691048548561 ) ) ;
#12128=EDGE_LOOP ( 'NONE', ( #7340, #36291 ) ) ;
#12208=DIRECTION ( 'NONE',  ( -0.000000000000000000, -0.000000000000000000, 1.000000000000000000 ) ) ;
#12255=VERTEX_POINT ( 'NONE', #6864 ) ;
#12273=CIRCLE ( 'NONE', #29067, 5.000000000000000888 ) ;
#12327=CARTESIAN_POINT ( 'NONE',  ( 4.592054218142288313, 3.122278952918447814, -5.689399939901071512 ) ) ;
#12402=DIRECTION ( 'NONE',  ( 0.000000000000000000, 0.000000000000000000, -1.000000000000000000 ) ) ;
#12454=CARTESIAN_POINT ( 'NONE',  ( 5.000000000000000888, 0.5616961504262232285, -0.5576671450146228892 ) ) ;
#12482=EDGE_LOOP ( 'NONE', ( #6558, #13714, #23137, #20124 ) ) ;
#12484=ADVANCED_FACE ( 'NONE', ( #9080 ), #31765, .F. ) ;
#12553=AXIS2_PLACEMENT_3D ( 'NONE', #267, #20158, #6268 ) ;
#12571=ADVANCED_FACE ( 'NONE', ( #35163 ), #20696, .T. ) ;
#12605=CARTESIAN_POINT ( 'NONE',  ( -0.9112620892301054321, -5.247385279376963751, -1.160540885688338131 ) ) ;
#12664=CARTESIAN_POINT ( 'NONE',  ( 5.000000000000000888, 0.9828435001097636237, -5.956909652965543422 ) ) ;
#12693=ORIENTED_EDGE ( 'NONE', *, *, #20415, .F. ) ;
#12715=CARTESIAN_POINT ( 'NONE',  ( -5.000000000000000000, -0.2835658343809315807, -0.5205273423269579647 ) ) ;
#12728=ORIENTED_EDGE ( 'NONE', *, *, #34398, .T. ) ;
#12853=LINE ( 'NONE', #7255, #22598 ) ;
#12864=AXIS2_PLACEMENT_3D ( 'NONE', #15249, #26688, #25957 ) ;
#12869=DIRECTION ( 'NONE',  ( -0.000000000000000000, -0.000000000000000000, 1.000000000000000000 ) ) ;
#12893=SHAPE_REPRESENTATION_RELATIONSHIP ( 'NONE' , 'NONE' ,  #35440, #30477 ) ;
#12922=CARTESIAN_POINT ( 'NONE',  ( -1.648146632869002426, -4.821944789745372439, -6.000000000000000000 ) ) ;
#12957=ORIENTED_EDGE ( 'NONE', *, *, #4655, .T. ) ;
#12960=CARTESIAN_POINT ( 'NONE',  ( -5.000000000000000000, -2.886751345948133540, -6.000000000000000000 ) ) ;
#12974=EDGE_CURVE ( 'NONE', #21666, #27114, #5271, .T. ) ;
#12990=CIRCLE ( 'NONE', #32151, 3.000000000000000000 ) ;
#13012=DIRECTION ( 'NONE',  ( 0.000000000000000000, -0.000000000000000000, 1.000000000000000000 ) ) ;
#13152=VERTEX_POINT ( 'NONE', #9984 ) ;
#13153=DIRECTION ( 'NONE',  ( 1.000000000000000000, 0.000000000000000000, 0.000000000000000000 ) ) ;
#13173=( GEOMETRIC_REPRESENTATION_CONTEXT ( 3 ) GLOBAL_UNCERTAINTY_ASSIGNED_CONTEXT ( ( #36927 ) ) GLOBAL_UNIT_ASSIGNED_CONTEXT ( ( #25929, #17859, #34755 ) ) REPRESENTATION_CONTEXT ( 'NONE', 'WORKASPACE' ) );
#13184=CIRCLE ( 'NONE', #13782, 5.000000000000000888 ) ;
#13202=EDGE_CURVE ( 'NONE', #26731, #23730, #3780, .T. ) ;
#13288=CARTESIAN_POINT ( 'NONE',  ( -5.000000000000000000, -1.349638343847294752, -0.8687551798607462405 ) ) ;
#13294=DIRECTION ( 'NONE',  ( -0.8191520442889917986, 1.003171929053524747E-16, 0.5735764363510460484 ) ) ;
#13298=CARTESIAN_POINT ( 'NONE',  ( -9.974659986866640793E-15, -5.773502691896262640, -5.553418012614792509 ) ) ;
#13308=LINE ( 'NONE', #16321, #3952 ) ;
#13310=CARTESIAN_POINT ( 'NONE',  ( 5.000000000000000888, -1.831125658499874742, -1.158123955083391943 ) ) ;
#13318=CARTESIAN_POINT ( 'NONE',  ( 0.9112620892300974385, 5.247385279376962863, -1.160540885688332136 ) ) ;
#13420=EDGE_CURVE ( 'NONE', #816, #17546, #5122, .T. ) ;
#13518=DIRECTION ( 'NONE',  ( 1.000000000000000000, 0.000000000000000000, 0.000000000000000000 ) ) ;
#13601=DIRECTION ( 'NONE',  ( -1.000000000000000000, 0.000000000000000000, 0.000000000000000000 ) ) ;
#13687=ORIENTED_EDGE ( 'NONE', *, *, #1217, .T. ) ;
#13714=ORIENTED_EDGE ( 'NONE', *, *, #32709, .F. ) ;
#13766=MECHANICAL_DESIGN_GEOMETRIC_PRESENTATION_REPRESENTATION('',(#33559),#13173);
#13782=AXIS2_PLACEMENT_3D ( 'NONE', #15687, #1614, #18688 ) ;
#13794=CARTESIAN_POINT ( 'NONE',  ( -2.500000000000003997, 4.330127018922192761, -6.000000000000000000 ) ) ;
#13804=CARTESIAN_POINT ( 'NONE',  ( 5.000000000000000000, 2.886751345948125991, -6.000000000000000000 ) ) ;
#13864=CARTESIAN_POINT ( 'NONE',  ( 4.999999999999999112, -0.2835658343809315252, -0.5205273423269578537 ) ) ;
#13871=CARTESIAN_POINT ( 'NONE',  ( -2.500000000000000000, 3.061616997868383141E-16, -6.000000000000000000 ) ) ;
#13903=CARTESIAN_POINT ( 'NONE',  ( -2.739742549670663330, -4.191711593333635300, -0.5197061503823270368 ) ) ;
#13959=CIRCLE ( 'NONE', #3176, 3.000000000000000000 ) ;
#13982=ORIENTED_EDGE ( 'NONE', *, *, #2930, .F. ) ;
#14092=AXIS2_PLACEMENT_3D ( 'NONE', #5935, #12072, #9486 ) ;
#14116=DIRECTION ( 'NONE',  ( -0.5000000000000006661, -0.8660254037844382635, 0.000000000000000000 ) ) ;
#14143=CARTESIAN_POINT ( 'NONE',  ( 4.652319770550017886, -3.087484620012992398, -1.687189089856322655 ) ) ;
#14196=AXIS2_PLACEMENT_3D ( 'NONE', #1440, #2190, #24528 ) ;
#14209=VECTOR ( 'NONE', #32535, 1000.000000000000000 ) ;
#14276=DIRECTION ( 'NONE',  ( -0.8191520442889890230, 0.000000000000000000, -0.5735764363510501562 ) ) ;
#14370=CARTESIAN_POINT ( 'NONE',  ( 1.301042606982605321E-15, 5.773502691896264416, -5.553418012614792509 ) ) ;
#14426=CARTESIAN_POINT ( 'NONE',  ( 1.653121499799246719, -4.819072548984012272, -5.948595712916168843 ) ) ;
#14480=DIRECTION ( 'NONE',  ( -0.000000000000000000, -0.000000000000000000, 1.000000000000000000 ) ) ;
#14515=ORIENTED_EDGE ( 'NONE', *, *, #4924, .T. ) ;
#14680=EDGE_CURVE ( 'NONE', #28024, #13152, #2976, .T. ) ;
#14723=CARTESIAN_POINT ( 'NONE',  ( 0.8179331680532997417, 5.301268757141563981, -5.826062401966623838 ) ) ;
#14790=CARTESIAN_POINT ( 'NONE',  ( 1.443735181952766844, -4.939961795957303003, -5.918341802876224911 ) ) ;
#14878=CARTESIAN_POINT ( 'NONE',  ( -3.000000000000000000, 3.673940397442059868E-16, -25.03750572909317285 ) ) ;
#14893=CARTESIAN_POINT ( 'NONE',  ( -1.084202172485504434E-14, -5.773502691896260863, -2.080000000000000071 ) ) ;
#14906=ORIENTED_EDGE ( 'NONE', *, *, #28480, .F. ) ;
#14913=EDGE_CURVE ( 'NONE', #9742, #32864, #5682, .T. ) ;
#14954=ORIENTED_EDGE ( 'NONE', *, *, #3861, .F. ) ;
#15020=CARTESIAN_POINT ( 'NONE',  ( -5.000000000000000000, 2.886751345948126879, -2.079999999999992077 ) ) ;
#15072=CARTESIAN_POINT ( 'NONE',  ( 4.088737910769899564, -3.412868758467433317, -1.160540885688329249 ) ) ;
#15101=CARTESIAN_POINT ( 'NONE',  ( 0.000000000000000000, 0.000000000000000000, -6.000000000000000000 ) ) ;
#15155=VERTEX_POINT ( 'NONE', #21289 ) ;
#15160=ORIENTED_EDGE ( 'NONE', *, *, #1840, .F. ) ;
#15192=CARTESIAN_POINT ( 'NONE',  ( -5.000000000000000000, 1.352381405509855972, -0.8629530094790016648 ) ) ;
#15216=ORIENTED_EDGE ( 'NONE', *, *, #12974, .F. ) ;
#15230=CARTESIAN_POINT ( 'NONE',  ( -2.008727693139930270, -4.613763217533273675, -0.5592653008974395323 ) ) ;
#15249=CARTESIAN_POINT ( 'NONE',  ( 6.078523336270777024E-16, 5.773502691896261751, -6.000000000000000000 ) ) ;
#15250=ORIENTED_EDGE ( 'NONE', *, *, #4924, .F. ) ;
#15384=CARTESIAN_POINT ( 'NONE',  ( -5.000000000000000000, -4.846777557549235459E-18, -0.5080592402122449114 ) ) ;
#15392=CARTESIAN_POINT ( 'NONE',  ( 3.351853367131008454, -3.838309248099023296, -6.000000000000000000 ) ) ;
#15403=DIRECTION ( 'NONE',  ( 1.000000000000000000, 0.000000000000000000, 0.000000000000000000 ) ) ;
#15404=CARTESIAN_POINT ( 'NONE',  ( 4.828573329308747830, 2.985724580418001928, -1.878862934774779836 ) ) ;
#15414=DIRECTION ( 'NONE',  ( 0.000000000000000000, 0.000000000000000000, -1.000000000000000000 ) ) ;
#15423=EDGE_LOOP ( 'NONE', ( #20402, #28021, #25070, #34420 ) ) ;
#15464=CONICAL_SURFACE ( 'NONE', #2298, 5.000000000000000888, 1.047197551196596299 ) ;
#15501=CARTESIAN_POINT ( 'NONE',  ( 5.000000000000000000, 2.886751345948137981, -5.553418012614792509 ) ) ;
#15511=DIRECTION ( 'NONE',  ( -1.000000000000000000, 0.000000000000000000, 0.000000000000000000 ) ) ;
#15595=EDGE_CURVE ( 'NONE', #28024, #26731, #16542, .T. ) ;
#15617=DIRECTION ( 'NONE',  ( 1.000000000000000000, 0.000000000000000000, 0.000000000000000000 ) ) ;
#15659=CARTESIAN_POINT ( 'NONE',  ( -5.000000000000000000, 0.000000000000000000, -6.000000000000000000 ) ) ;
#15678=LINE ( 'NONE', #27482, #14209 ) ;
#15687=CARTESIAN_POINT ( 'NONE',  ( 0.000000000000000000, 0.000000000000000000, -6.000000000000000000 ) ) ;
#15769=CARTESIAN_POINT ( 'NONE',  ( 2.008727693139922721, 4.613763217533267458, -0.5592653008974296514 ) ) ;
#15784=DIRECTION ( 'NONE',  ( 0.000000000000000000, 0.000000000000000000, 1.000000000000000000 ) ) ;
#15796=CARTESIAN_POINT ( 'NONE',  ( -1.084202172485504434E-14, -5.773502691896260863, -2.080000000000000071 ) ) ;
#15833=DIRECTION ( 'NONE',  ( -1.000000000000000000, 0.000000000000000000, 0.000000000000000000 ) ) ;
#15966=DIRECTION ( 'NONE',  ( -0.000000000000000000, -0.000000000000000000, 1.000000000000000000 ) ) ;
#15972=EDGE_CURVE ( 'NONE', #10440, #4982, #25894, .T. ) ;
#16089=CARTESIAN_POINT ( 'NONE',  ( 3.035766082959412415E-15, 5.773502691896260863, -2.080000000000000071 ) ) ;
#16121=ORIENTED_EDGE ( 'NONE', *, *, #7869, .T. ) ;
#16126=ORIENTED_EDGE ( 'NONE', *, *, #2684, .F. ) ;
#16162=DIRECTION ( 'NONE',  ( 0.5000000000000006661, -0.8660254037844383745, 0.000000000000000000 ) ) ;
#16183=COLOUR_RGB ( '', 0.31764706, 0.68627451, 0.89019608) ;
#16185=CARTESIAN_POINT ( 'NONE',  ( -2.981146944884250694, -4.052336700773510714, -0.5666985376598571156 ) ) ;
#16321=CARTESIAN_POINT ( 'NONE',  ( 4.749999999999999112, 5.817072295949926440E-16, 0.000000000000000000 ) ) ;
#16335=B_SPLINE_CURVE_WITH_KNOTS ( 'NONE', 3,
 ( #18086, #32512, #12454, #35535, #29512, #27078, #1389, #24264, #23923, #35375 ),
 .UNSPECIFIED., .F., .F.,
 ( 4, 2, 2, 2, 4 ),
 ( 0.01815567983891738443, 0.01899359644517026671, 0.01983151305142315246, 0.02066942965767603474, 0.02150734626392891702 ),
 .UNSPECIFIED. ) ;
#16438=CARTESIAN_POINT ( 'NONE',  ( 0.000000000000000000, 0.000000000000000000, -5.624496230895140947 ) ) ;
#16476=AXIS2_PLACEMENT_3D ( 'NONE', #25408, #19411, #13601 ) ;
#16542=B_SPLINE_CURVE_WITH_KNOTS ( 'NONE', 3,
 ( #34048, #19794, #14143, #23897, #15072, #9456, #8897, #28935, #20684, #31756, #11881, #6083, #17692, #32114, #29127, #26139, #29488, #6256, #3462, #14893 ),
 .UNSPECIFIED., .F., .F.,
 ( 4, 2, 2, 2, 2, 2, 2, 2, 2, 4 ),
 ( 2.781148944256651962E-07, 0.0008372784139787452749, 0.001674278713063064939, 0.002511279012147384603, 0.003348279311231704483, 0.003766779460773864857, 0.004185279610316025231, 0.005022279909400345112, 0.005859280208484664992, 0.006696280507568985740 ),
 .UNSPECIFIED. ) ;
#16544=CARTESIAN_POINT ( 'NONE',  ( -4.828573329308746942, -2.985724580418009921, -1.878862934774787830 ) ) ;
#16578=ORIENTED_EDGE ( 'NONE', *, *, #28428, .T. ) ;
#16609=CARTESIAN_POINT ( 'NONE',  ( 3.000000000000000000, 3.673940397442059868E-16, -5.974599999999999689 ) ) ;
#16635=CARTESIAN_POINT ( 'NONE',  ( -4.282125186551308360, 3.301216562737181892, -1.327869168827478408 ) ) ;
#16649=CARTESIAN_POINT ( 'NONE',  ( -4.182066831946699814, 3.358985280702823761, -5.826062401966626503 ) ) ;
#16664=CARTESIAN_POINT ( 'NONE',  ( -5.000000000000000000, -2.886751345948137981, -5.553418012614792509 ) ) ;
#16670=VERTEX_POINT ( 'NONE', #23297 ) ;
#16790=VERTEX_POINT ( 'NONE', #29452 ) ;
#16798=CARTESIAN_POINT ( 'NONE',  ( -1.443735181952766622, 4.939961795957295898, -5.918341802876230240 ) ) ;
#16868=EDGE_CURVE ( 'NONE', #4982, #32183, #9281, .T. ) ;
#16877=DIRECTION ( 'NONE',  ( 0.000000000000000000, 0.000000000000000000, 1.000000000000000000 ) ) ;
#16936=PRODUCT_DEFINITION_SHAPE ( 'NONE', 'NONE',  #9065 ) ;
#17026=FACE_BOUND ( 'NONE', #17092, .T. ) ;
#17041=B_SPLINE_CURVE_WITH_KNOTS ( 'NONE', 3,
 ( #29018, #34856, #29220, #14426, #14790, #6343, #34307, #2813 ),
 .UNSPECIFIED., .F., .F.,
 ( 4, 2, 2, 4 ),
 ( 0.002921158011986708155, 0.003648658599403065313, 0.004376159186819422037, 0.005831160361652136352 ),
 .UNSPECIFIED. ) ;
#17092=EDGE_LOOP ( 'NONE', ( #22287, #4069 ) ) ;
#17108=ADVANCED_FACE ( 'NONE', ( #19841 ), #30347, .F. ) ;
#17241=DIRECTION ( 'NONE',  ( 0.000000000000000000, 0.000000000000000000, 1.000000000000000000 ) ) ;
#17261=VECTOR ( 'NONE', #29736, 1000.000000000000000 ) ;
#17268=B_SPLINE_CURVE_WITH_KNOTS ( 'NONE', 3,
 ( #36368, #35821, #7866, #21364, #27557, #24926, #13288, #10476, #26988, #9918, #1679, #12715, #18570, #24170 ),
 .UNSPECIFIED., .F., .F.,
 ( 4, 2, 2, 2, 2, 2, 4 ),
 ( 0.01481111731982464805, 0.01564725794959783214, 0.01648339857937101624, 0.01690146889425760829, 0.01731953920914420034, 0.01773760952403079239, 0.01815567983891738443 ),
 .UNSPECIFIED. ) ;
#17276=DIRECTION ( 'NONE',  ( -0.000000000000000000, -0.000000000000000000, 1.000000000000000000 ) ) ;
#17301=CARTESIAN_POINT ( 'NONE',  ( 0.000000000000000000, 0.000000000000000000, -5.974599999999999689 ) ) ;
#17497=B_SPLINE_CURVE_WITH_KNOTS ( 'NONE', 3,
 ( #33648, #19385, #30804, #10581, #28014, #4401 ),
 .UNSPECIFIED., .F., .F.,
 ( 4, 2, 4 ),
 ( 0.005150343764683549923, 0.006610526168996381374, 0.008070708573309213693 ),
 .UNSPECIFIED. ) ;
#17546=VERTEX_POINT ( 'NONE', #6476 ) ;
#17553=PRODUCT_CONTEXT ( 'NONE', #5099, 'mechanical' ) ;
#17603=CIRCLE ( 'NONE', #24201, 3.000000000000000000 ) ;
#17619=ORIENTED_EDGE ( 'NONE', *, *, #28372, .F. ) ;
#17672=CIRCLE ( 'NONE', #16476, 3.000000000000000000 ) ;
#17692=CARTESIAN_POINT ( 'NONE',  ( 1.898848305348270982, -4.677202111653177674, -0.6020238742160556322 ) ) ;
#17725=DIRECTION ( 'NONE',  ( 0.8191520442889917986, 0.000000000000000000, 0.5735764363510460484 ) ) ;
#17758=MECHANICAL_DESIGN_GEOMETRIC_PRESENTATION_REPRESENTATION('',(#33323),#20750);
#17839=DIRECTION ( 'NONE',  ( -0.000000000000000000, -0.000000000000000000, 1.000000000000000000 ) ) ;
#17859=( NAMED_UNIT ( * ) PLANE_ANGLE_UNIT ( ) SI_UNIT ( $, .RADIAN. ) );
#17985=CARTESIAN_POINT ( 'NONE',  ( 2.500000000000005773, 4.330127018922191873, -6.000000000000000000 ) ) ;
#18011=ADVANCED_FACE ( 'NONE', ( #6967, #18418 ), #6414, .F. ) ;
#18040=PRESENTATION_STYLE_ASSIGNMENT (( #8675 ) ) ;
#18073=CARTESIAN_POINT ( 'NONE',  ( 5.000000000000000000, -2.886751345948134428, -6.000000000000000000 ) ) ;
#18086=CARTESIAN_POINT ( 'NONE',  ( 5.000000000000000000, 6.074766241781102566E-16, -0.5080592402122449114 ) ) ;
#18121=CARTESIAN_POINT ( 'NONE',  ( 0.000000000000000000, 0.000000000000000000, -5.974599999999999689 ) ) ;
#18196=CONICAL_SURFACE ( 'NONE', #854, 5.000000000000000888, 1.047197551196596299 ) ;
#18199=CARTESIAN_POINT ( 'NONE',  ( 3.101151694651712809, 3.983051926191225611, -0.6020238742160355372 ) ) ;
#18215=ORIENTED_EDGE ( 'NONE', *, *, #33218, .T. ) ;
#18297=CARTESIAN_POINT ( 'NONE',  ( 5.000000000000000000, 1.947085426416884202, -5.800379292880308846 ) ) ;
#18386=CLOSED_SHELL ( 'NONE', ( #25004, #17108, #26279, #20220, #12484, #35257, #10769, #20408, #32840, #12571, #19049, #34487, #18011, #1890, #31167, #2607, #566, #21342, #20529, #8958, #30914, #5474, #34146, #31853 ) ) ;
#18418=FACE_OUTER_BOUND ( 'NONE', #28509, .T. ) ;
#18476=ORIENTED_EDGE ( 'NONE', *, *, #11798, .F. ) ;
#18530=APPLICATION_CONTEXT ( 'automotive_design' ) ;
#18555=EDGE_CURVE ( 'NONE', #23730, #816, #17268, .T. ) ;
#18570=CARTESIAN_POINT ( 'NONE',  ( -5.000000000000000000, -0.1416384297035285789, -0.5080592402122394713 ) ) ;
#18581=CARTESIAN_POINT ( 'NONE',  ( -2.500000000000003997, -4.330127018922192761, -6.000000000000000000 ) ) ;
#18589=EDGE_LOOP ( 'NONE', ( #8919, #5974, #12957, #7362, #26811, #22632 ) ) ;
#18599=CARTESIAN_POINT ( 'NONE',  ( 4.279208249584789847, 3.302900657080011459, -1.325189086772932123 ) ) ;
#18676=CARTESIAN_POINT ( 'NONE',  ( -3.000000000000000000, 3.673940397442059868E-16, 0.000000000000000000 ) ) ;
#18688=DIRECTION ( 'NONE',  ( 1.000000000000000000, 0.000000000000000000, 0.000000000000000000 ) ) ;
#18701=AXIS2_PLACEMENT_3D ( 'NONE', #32460, #15414, #20848 ) ;
#18760=CARTESIAN_POINT ( 'NONE',  ( -2.500000000000003997, -4.330127018922192761, -6.000000000000000000 ) ) ;
#18800=CARTESIAN_POINT ( 'NONE',  ( -3.447886558751868336, -3.782864459065579776, -0.7348938709837913308 ) ) ;
#18830=EDGE_CURVE ( 'NONE', #13152, #12255, #16335, .T. ) ;
#18843=ORIENTED_EDGE ( 'NONE', *, *, #19294, .T. ) ;
#18863=CARTESIAN_POINT ( 'NONE',  ( 4.999999999999999112, 0.4881033300985041512, -6.000000000000000000 ) ) ;
#18951=CARTESIAN_POINT ( 'NONE',  ( 5.000000000000000000, -0.6964580643377611402, -0.6026403643956901313 ) ) ;
#18963=CARTESIAN_POINT ( 'NONE',  ( 1.546821644788039851, 4.880444798889544522, -0.7375898304884582757 ) ) ;
#18990=PLANE ( 'NONE',  #21706 ) ;
#18992=CARTESIAN_POINT ( 'NONE',  ( -2.255011273957059359, -4.471571325851515510, -0.5083873451168858804 ) ) ;
#19004=CIRCLE ( 'NONE', #25585, 4.749999999999999112 ) ;
#19037=FACE_OUTER_BOUND ( 'NONE', #18589, .T. ) ;
#19049=ADVANCED_FACE ( 'NONE', ( #420 ), #29094, .T. ) ;
#19059=CARTESIAN_POINT ( 'NONE',  ( -4.749999999999999112, 0.000000000000000000, 0.000000000000000000 ) ) ;
#19203=CIRCLE ( 'NONE', #23984, 5.000000000000000888 ) ;
#19285=SURFACE_STYLE_USAGE ( .BOTH. , #1459 ) ;
#19294=EDGE_CURVE ( 'NONE', #21710, #16670, #27164, .T. ) ;
#19352=CARTESIAN_POINT ( 'NONE',  ( -4.279208249584786294, -3.302900657080020341, -1.325189086772939895 ) ) ;
#19385=CARTESIAN_POINT ( 'NONE',  ( -4.999999999999999112, -2.417244626924490269, -5.688952927922134251 ) ) ;
#19411=DIRECTION ( 'NONE',  ( 0.000000000000000000, -0.000000000000000000, 1.000000000000000000 ) ) ;
#19438=CARTESIAN_POINT ( 'NONE',  ( -2.018853055115723105, 4.607917337070899677, -0.5666985376598566715 ) ) ;
#19459=DIRECTION ( 'NONE',  ( 1.000000000000000000, 0.000000000000000000, 0.000000000000000000 ) ) ;
#19520=EDGE_CURVE ( 'NONE', #36720, #9972, #17603, .T. ) ;
#19559=ORIENTED_EDGE ( 'NONE', *, *, #14680, .T. ) ;
#19794=CARTESIAN_POINT ( 'NONE',  ( 4.829002333675111558, -2.985476894631607259, -1.879366290983715881 ) ) ;
#19816=B_SPLINE_CURVE_WITH_KNOTS ( 'NONE', 3,
 ( #17985, #32792, #9153, #20584, #20785, #1107, #12327, #29409 ),
 .UNSPECIFIED., .F., .F.,
 ( 4, 2, 2, 4 ),
 ( 0.002921158011986721599, 0.003648658599403073119, 0.004376159186819424639, 0.005831160361652126811 ),
 .UNSPECIFIED. ) ;
#19841=FACE_OUTER_BOUND ( 'NONE', #8114, .T. ) ;
#20095=DIRECTION ( 'NONE',  ( -0.8660254037844380415, 0.5000000000000008882, 0.000000000000000000 ) ) ;
#20106=EDGE_CURVE ( 'NONE', #16790, #12255, #7810, .T. ) ;
#20124=ORIENTED_EDGE ( 'NONE', *, *, #33218, .F. ) ;
#20158=DIRECTION ( 'NONE',  ( 0.000000000000000000, 0.000000000000000000, 1.000000000000000000 ) ) ;
#20171=VERTEX_POINT ( 'NONE', #11518 ) ;
#20220=ADVANCED_FACE ( 'NONE', ( #22602 ), #8012, .T. ) ;
#20280=CARTESIAN_POINT ( 'NONE',  ( 5.000000000000000888, -1.936377641173859798, -5.802630826755080129 ) ) ;
#20402=ORIENTED_EDGE ( 'NONE', *, *, #11798, .T. ) ;
#20408=ADVANCED_FACE ( 'NONE', ( #1801 ), #28339, .T. ) ;
#20415=EDGE_CURVE ( 'NONE', #16670, #21710, #31363, .T. ) ;
#20425=VERTEX_POINT ( 'NONE', #19059 ) ;
#20444=ORIENTED_EDGE ( 'NONE', *, *, #4655, .F. ) ;
#20451=CARTESIAN_POINT ( 'NONE',  ( 3.000000000000000000, 0.000000000000000000, 0.000000000000000000 ) ) ;
#20466=CARTESIAN_POINT ( 'NONE',  ( -5.000000000000000000, -2.886751345948134428, -2.080000000000000071 ) ) ;
#20529=ADVANCED_FACE ( 'NONE', ( #26284 ), #18196, .T. ) ;
#20535=AXIS2_PLACEMENT_3D ( 'NONE', #9331, #17241, #5990 ) ;
#20584=CARTESIAN_POINT ( 'NONE',  ( 3.346878500200757944, 3.841181488860379911, -5.948595712916174172 ) ) ;
#20624=VECTOR ( 'NONE', #30661, 1000.000000000000000 ) ;
#20684=CARTESIAN_POINT ( 'NONE',  ( 2.744988726042924210, -4.188682711992893992, -0.5083873451168847701 ) ) ;
#20696=PLANE ( 'NONE',  #1811 ) ;
#20750=( GEOMETRIC_REPRESENTATION_CONTEXT ( 3 ) GLOBAL_UNCERTAINTY_ASSIGNED_CONTEXT ( ( #10695 ) ) GLOBAL_UNIT_ASSIGNED_CONTEXT ( ( #4291, #27143, #33548 ) ) REPRESENTATION_CONTEXT ( 'NONE', 'WORKASPACE' ) );
#20777=ORIENTED_EDGE ( 'NONE', *, *, #1803, .F. ) ;
#20785=CARTESIAN_POINT ( 'NONE',  ( 3.556264818047235821, 3.720292241887089624, -5.918341802876230240 ) ) ;
#20821=CARTESIAN_POINT ( 'NONE',  ( -4.999999999999999112, 0.2838785441256745923, -0.5080592402122393603 ) ) ;
#20848=DIRECTION ( 'NONE',  ( -1.000000000000000000, 0.000000000000000000, 0.000000000000000000 ) ) ;
#20871=CARTESIAN_POINT ( 'NONE',  ( -1.324703144935793775, -5.008684974571242066, -0.8655517945778401501 ) ) ;
#20880=ORIENTED_EDGE ( 'NONE', *, *, #1217, .F. ) ;
#21011=CARTESIAN_POINT ( 'NONE',  ( -5.000000000000000000, 1.101175676120956348, -0.7375066809288767233 ) ) ;
#21075=ORIENTED_EDGE ( 'NONE', *, *, #16868, .T. ) ;
#21099=CARTESIAN_POINT ( 'NONE',  ( -5.000000000000000000, 0.000000000000000000, -6.000000000000000000 ) ) ;
#21199=CARTESIAN_POINT ( 'NONE',  ( 3.667169054266697703, 3.656261651251516032, -0.8603634151101352545 ) ) ;
#21252=ORIENTED_EDGE ( 'NONE', *, *, #20415, .T. ) ;
#21276=FACE_OUTER_BOUND ( 'NONE', #11522, .T. ) ;
#21289=CARTESIAN_POINT ( 'NONE',  ( 4.749999999999999112, 6.447547231611302361E-16, 0.000000000000000000 ) ) ;
#21338=EDGE_LOOP ( 'NONE', ( #15250, #5522, #32870, #33979, #3757, #26440, #19559 ) ) ;
#21342=ADVANCED_FACE ( 'NONE', ( #5020 ), #8700, .T. ) ;
#21346=CARTESIAN_POINT ( 'NONE',  ( 0.000000000000000000, 0.000000000000000000, -0.3501037691048548561 ) ) ;
#21356=ORIENTED_EDGE ( 'NONE', *, *, #6112, .T. ) ;
#21364=CARTESIAN_POINT ( 'NONE',  ( -4.999999999999998224, -2.058885705017527989, -1.328630925609301183 ) ) ;
#21385=AXIS2_PLACEMENT_3D ( 'NONE', #8896, #30384, #36396 ) ;
#21398=CARTESIAN_POINT ( 'NONE',  ( 2.739742549670660665, 4.191711593333631747, -0.5197061503823161566 ) ) ;
#21553=CARTESIAN_POINT ( 'NONE',  ( -1.084202172485504434E-14, -5.773502691896260863, -2.080000000000000071 ) ) ;
#21599=ORIENTED_EDGE ( 'NONE', *, *, #2684, .T. ) ;
#21609=DIRECTION ( 'NONE',  ( -0.000000000000000000, -0.000000000000000000, 1.000000000000000000 ) ) ;
#21612=CARTESIAN_POINT ( 'NONE',  ( 0.000000000000000000, 0.000000000000000000, -0.3501037691048548561 ) ) ;
#21666=VERTEX_POINT ( 'NONE', #7249 ) ;
#21706=AXIS2_PLACEMENT_3D ( 'NONE', #1916, #30418, #4747 ) ;
#21710=VERTEX_POINT ( 'NONE', #16609 ) ;
#21753=ORIENTED_EDGE ( 'NONE', *, *, #36993, .T. ) ;
#21757=CARTESIAN_POINT ( 'NONE',  ( 3.035766082959412415E-15, 5.773502691896260863, -2.080000000000000071 ) ) ;
#21876=CARTESIAN_POINT ( 'NONE',  ( -1.898848305348268983, 4.677202111653171457, -0.6020238742160447520 ) ) ;
#21895=CARTESIAN_POINT ( 'NONE',  ( -5.000000000000000000, 2.886751345948137981, -5.553418012614792509 ) ) ;
#21951=AXIS2_PLACEMENT_3D ( 'NONE', #21612, #12402, #15617 ) ;
#22035=EDGE_CURVE ( 'NONE', #35263, #28024, #29884, .T. ) ;
#22081=CARTESIAN_POINT ( 'NONE',  ( -0.1714266706912549731, 5.674529457426383594, -1.878862934774786275 ) ) ;
#22100=B_SPLINE_CURVE_WITH_KNOTS ( 'NONE', 3,
 ( #9194, #32047, #15392, #27382 ),
 .UNSPECIFIED., .F., .F.,
 ( 4, 4 ),
 ( 2.380735200807732181E-07, 0.002921158011986708155 ),
 .UNSPECIFIED. ) ;
#22125=DIRECTION ( 'NONE',  ( 0.000000000000000000, 0.000000000000000000, -1.000000000000000000 ) ) ;
#22257=CARTESIAN_POINT ( 'NONE',  ( -0.7207917504152121513, 5.357353380764376283, -1.325189086772940117 ) ) ;
#22287=ORIENTED_EDGE ( 'NONE', *, *, #28480, .T. ) ;
#22317=LINE ( 'NONE', #13871, #34565 ) ;
#22347=ORIENTED_EDGE ( 'NONE', *, *, #486, .T. ) ;
#22564=AXIS2_PLACEMENT_3D ( 'NONE', #18121, #24310, #15511 ) ;
#22598=VECTOR ( 'NONE', #1983, 999.9999999999998863 ) ;
#22602=FACE_OUTER_BOUND ( 'NONE', #33657, .T. ) ;
#22632=ORIENTED_EDGE ( 'NONE', *, *, #18830, .F. ) ;
#22658=CARTESIAN_POINT ( 'NONE',  ( -2.925285743277526329, -4.084588180558410109, -5.989444439476605986 ) ) ;
#22803=DIRECTION ( 'NONE',  ( 0.000000000000000000, 0.000000000000000000, -1.000000000000000000 ) ) ;
#22864=EDGE_CURVE ( 'NONE', #9742, #17546, #32744, .T. ) ;
#22947=DIRECTION ( 'NONE',  ( -0.000000000000000000, -0.000000000000000000, 1.000000000000000000 ) ) ;
#22992=LINE ( 'NONE', #34432, #36227 ) ;
#23015=ORIENTED_EDGE ( 'NONE', *, *, #30558, .F. ) ;
#23119=CARTESIAN_POINT ( 'NONE',  ( 2.500000000000005773, 4.330127018922191873, -6.000000000000000000 ) ) ;
#23137=ORIENTED_EDGE ( 'NONE', *, *, #36866, .T. ) ;
#23217=DIRECTION ( 'NONE',  ( -0.000000000000000000, -0.000000000000000000, 1.000000000000000000 ) ) ;
#23220=VECTOR ( 'NONE', #17725, 1000.000000000000227 ) ;
#23245=CIRCLE ( 'NONE', #33430, 5.000000000000000888 ) ;
#23297=CARTESIAN_POINT ( 'NONE',  ( -3.000000000000000000, 0.000000000000000000, -5.974599999999999689 ) ) ;
#23312=DIRECTION ( 'NONE',  ( 0.8660254037844382635, -0.5000000000000006661, 0.000000000000000000 ) ) ;
#23353=EDGE_LOOP ( 'NONE', ( #7409, #25689, #20444 ) ) ;
#23456=CARTESIAN_POINT ( 'NONE',  ( -4.999999999999999112, 2.059541880721995177, -1.329159518034682685 ) ) ;
#23656=ORIENTED_EDGE ( 'NONE', *, *, #3861, .T. ) ;
#23664=FILL_AREA_STYLE_COLOUR ( '', #16183 ) ;
#23677=CARTESIAN_POINT ( 'NONE',  ( -0.1709976663249050954, -5.674777143212785369, -1.879366290983713217 ) ) ;
#23697=FACE_OUTER_BOUND ( 'NONE', #1546, .T. ) ;
#23730=VERTEX_POINT ( 'NONE', #20466 ) ;
#23897=CARTESIAN_POINT ( 'NONE',  ( 4.282125186551308360, -3.301216562737187221, -1.327869168827487290 ) ) ;
#23923=CARTESIAN_POINT ( 'NONE',  ( 5.000000000000000000, 2.691270400161075216, -1.881368198414912429 ) ) ;
#23984=AXIS2_PLACEMENT_3D ( 'NONE', #35322, #6426, #26865 ) ;
#23990=DIRECTION ( 'NONE',  ( -0.000000000000000000, -0.000000000000000000, 1.000000000000000000 ) ) ;
#24038=DIRECTION ( 'NONE',  ( -1.000000000000000000, 0.000000000000000000, 0.000000000000000000 ) ) ;
#24059=CARTESIAN_POINT ( 'NONE',  ( -1.546821644788046735, -4.880444798889548963, -0.7375898304884659362 ) ) ;
#24074=ORIENTED_EDGE ( 'NONE', *, *, #15972, .F. ) ;
#24106=CARTESIAN_POINT ( 'NONE',  ( -5.000000000000000000, 1.947085426416883980, -5.800379292880308846 ) ) ;
#24156=( NAMED_UNIT ( * ) PLANE_ANGLE_UNIT ( ) SI_UNIT ( $, .RADIAN. ) );
#24170=CARTESIAN_POINT ( 'NONE',  ( -5.000000000000000000, -4.846777557549235459E-18, -0.5080592402122449114 ) ) ;
#24201=AXIS2_PLACEMENT_3D ( 'NONE', #8822, #17276, #3029 ) ;
#24227=DIRECTION ( 'NONE',  ( 1.000000000000000000, 0.000000000000000000, 0.000000000000000000 ) ) ;
#24261=CARTESIAN_POINT ( 'NONE',  ( 0.000000000000000000, 0.000000000000000000, -6.000000000000000000 ) ) ;
#24263=AXIS2_PLACEMENT_3D ( 'NONE', #1974, #32735, #7061 ) ;
#24264=CARTESIAN_POINT ( 'NONE',  ( 5.000000000000000000, 2.488344183252611419, -1.689918788536298289 ) ) ;
#24296=CARTESIAN_POINT ( 'NONE',  ( 5.000000000000000000, 2.419979747126332903, -5.688163366729713566 ) ) ;
#24302=CIRCLE ( 'NONE', #14092, 2.500000000000000000 ) ;
#24310=DIRECTION ( 'NONE',  ( 0.000000000000000000, 0.000000000000000000, -1.000000000000000000 ) ) ;
#24405=CARTESIAN_POINT ( 'NONE',  ( 5.000000000000000000, 2.886751345948134428, -2.080000000000000071 ) ) ;
#24448=VERTEX_POINT ( 'NONE', #31760 ) ;
#24528=DIRECTION ( 'NONE',  ( 1.000000000000000000, 0.000000000000000000, 0.000000000000000000 ) ) ;
#24573=B_SPLINE_CURVE_WITH_KNOTS ( 'NONE', 3,
 ( #1805, #18863, #12664, #18297, #24296, #15501 ),
 .UNSPECIFIED., .F., .F.,
 ( 4, 2, 4 ),
 ( 0.008070708573309213693, 0.009531758523483289253, 0.01099280847365736308 ),
 .UNSPECIFIED. ) ;
#24606=EDGE_LOOP ( 'NONE', ( #11419, #10120, #9033, #36760 ) ) ;
#24627=CARTESIAN_POINT ( 'NONE',  ( -3.667169054266697259, -3.656261651251520917, -0.8603634151101461347 ) ) ;
#24634=ORIENTED_EDGE ( 'NONE', *, *, #34398, .F. ) ;
#24664=VERTEX_POINT ( 'NONE', #1204 ) ;
#24703=CARTESIAN_POINT ( 'NONE',  ( -0.3487148583350038744, 5.572172074566123179, -1.686035282245269995 ) ) ;
#24727=ORIENTED_EDGE ( 'NONE', *, *, #8002, .T. ) ;
#24757=CARTESIAN_POINT ( 'NONE',  ( 5.000000000000000000, -0.5603747650654238299, -0.5678343202077608121 ) ) ;
#24836=CARTESIAN_POINT ( 'NONE',  ( 5.000000000000000000, 2.886751345948125991, -6.000000000000000000 ) ) ;
#24857=CARTESIAN_POINT ( 'NONE',  ( -2.074714256722481664, 4.575665857285980742, -5.989444439476608650 ) ) ;
#24926=CARTESIAN_POINT ( 'NONE',  ( -5.000000000000000000, -1.472375319565265794, -0.9369361380397573935 ) ) ;
#24949=EDGE_CURVE ( 'NONE', #33082, #16790, #19816, .T. ) ;
#24993=CARTESIAN_POINT ( 'NONE',  ( -2.618768541235303005, -4.261555969668739507, -0.5078976954042990766 ) ) ;
#25004=ADVANCED_FACE ( 'NONE', ( #3729 ), #26594, .F. ) ;
#25070=ORIENTED_EDGE ( 'NONE', *, *, #19520, .T. ) ;
#25147=CARTESIAN_POINT ( 'NONE',  ( 5.000000000000000000, -2.058885705017528878, -1.328630925609301183 ) ) ;
#25234=CARTESIAN_POINT ( 'NONE',  ( -2.287832656137188891, 4.452621892014637872, -6.000000000000004441 ) ) ;
#25408=CARTESIAN_POINT ( 'NONE',  ( 0.000000000000000000, 0.000000000000000000, -6.000000000000001776 ) ) ;
#25430=CARTESIAN_POINT ( 'NONE',  ( -1.332830945733270545, 5.003992386592893915, -0.8603634151101617888 ) ) ;
#25444=EDGE_CURVE ( 'NONE', #28959, #33082, #13184, .T. ) ;
#25523=CARTESIAN_POINT ( 'NONE',  ( -3.000000000000000000, 0.000000000000000000, -5.974599999999999689 ) ) ;
#25543=CARTESIAN_POINT ( 'NONE',  ( -5.000000000000000000, 2.886751345948137981, -5.553418012614792509 ) ) ;
#25585=AXIS2_PLACEMENT_3D ( 'NONE', #30316, #12869, #29954 ) ;
#25614=EDGE_LOOP ( 'NONE', ( #15216, #22347, #18476, #34590 ) ) ;
#25689=ORIENTED_EDGE ( 'NONE', *, *, #1840, .T. ) ;
#25738=CARTESIAN_POINT ( 'NONE',  ( 5.000000000000000000, -0.9724665692850895660, -5.958069561147902427 ) ) ;
#25813=CARTESIAN_POINT ( 'NONE',  ( 2.500000000000005773, 4.330127018922191873, -6.000000000000000000 ) ) ;
#25817=VECTOR ( 'NONE', #11566, 999.9999999999998863 ) ;
#25894=B_SPLINE_CURVE_WITH_KNOTS ( 'NONE', 3,
 ( #13298, #7137, #12922, #18581 ),
 .UNSPECIFIED., .F., .F.,
 ( 4, 4 ),
 ( 2.380735200943099693E-07, 0.002921158011986722466 ),
 .UNSPECIFIED. ) ;
#25929=( LENGTH_UNIT ( ) NAMED_UNIT ( * ) SI_UNIT ( .MILLI., .METRE. ) );
#25943=FACE_OUTER_BOUND ( 'NONE', #35632, .T. ) ;
#25957=DIRECTION ( 'NONE',  ( -0.8660254037844382635, -0.5000000000000006661, 0.000000000000000000 ) ) ;
#26116=ORIENTED_EDGE ( 'NONE', *, *, #18830, .T. ) ;
#26139=CARTESIAN_POINT ( 'NONE',  ( 0.9154378789997317245, -5.244974386029391589, -1.156968425231173381 ) ) ;
#26166=CARTESIAN_POINT ( 'NONE',  ( 1.648146632868999539, 4.821944789745367110, -6.000000000000003553 ) ) ;
#26212=LINE ( 'NONE', #319, #25817 ) ;
#26248=ORIENTED_EDGE ( 'NONE', *, *, #15595, .T. ) ;
#26279=ADVANCED_FACE ( 'NONE', ( #27195 ), #5831, .F. ) ;
#26284=FACE_OUTER_BOUND ( 'NONE', #2740, .T. ) ;
#26318=LINE ( 'NONE', #14878, #33734 ) ;
#26440=ORIENTED_EDGE ( 'NONE', *, *, #15595, .F. ) ;
#26594=CYLINDRICAL_SURFACE ( 'NONE', #4149, 3.000000000000000000 ) ;
#26688=DIRECTION ( 'NONE',  ( -0.5000000000000006661, 0.8660254037844382635, 0.000000000000000000 ) ) ;
#26731=VERTEX_POINT ( 'NONE', #21553 ) ;
#26784=CARTESIAN_POINT ( 'NONE',  ( -9.974659986866640793E-15, -5.773502691896262640, -5.553418012614792509 ) ) ;
#26811=ORIENTED_EDGE ( 'NONE', *, *, #20106, .T. ) ;
#26865=DIRECTION ( 'NONE',  ( -1.000000000000000000, 0.000000000000000000, 0.000000000000000000 ) ) ;
#26875=CARTESIAN_POINT ( 'NONE',  ( -0.3476802294499993229, -5.572769417831399785, -1.687189089856318880 ) ) ;
#26908=DIRECTION ( 'NONE',  ( 0.000000000000000000, -0.000000000000000000, 1.000000000000000000 ) ) ;
#26968=ORIENTED_EDGE ( 'NONE', *, *, #10333, .F. ) ;
#26988=CARTESIAN_POINT ( 'NONE',  ( -5.000000000000000000, -0.9645339558193164464, -0.6919071587033235327 ) ) ;
#27001=DIRECTION ( 'NONE',  ( -0.000000000000000000, -0.000000000000000000, 1.000000000000000000 ) ) ;
#27078=CARTESIAN_POINT ( 'NONE',  ( 5.000000000000000000, 1.831554690317580780, -1.158389257021584795 ) ) ;
#27114=VERTEX_POINT ( 'NONE', #657 ) ;
#27143=( NAMED_UNIT ( * ) PLANE_ANGLE_UNIT ( ) SI_UNIT ( $, .RADIAN. ) );
#27164=CIRCLE ( 'NONE', #32544, 3.000000000000000000 ) ;
#27195=FACE_OUTER_BOUND ( 'NONE', #15423, .T. ) ;
#27251=EDGE_CURVE ( 'NONE', #32864, #29787, #12273, .T. ) ;
#27273=CARTESIAN_POINT ( 'NONE',  ( -4.999999999999999112, 0.4881033300985041512, -6.000000000000000000 ) ) ;
#27382=CARTESIAN_POINT ( 'NONE',  ( 2.500000000000003109, -4.330127018922192761, -6.000000000000000000 ) ) ;
#27384=CARTESIAN_POINT ( 'NONE',  ( 5.000000000000000000, -1.349638343847295419, -0.8687551798607463516 ) ) ;
#27409=CONICAL_SURFACE ( 'NONE', #33914, 3.000000000000000000, 0.9599310885968762586 ) ;
#27482=CARTESIAN_POINT ( 'NONE',  ( 2.500000000000000000, 0.000000000000000000, -6.000000000000000000 ) ) ;
#27543=CARTESIAN_POINT ( 'NONE',  ( -4.592054218142291866, -3.122278952918454031, -5.689399939901067071 ) ) ;
#27557=CARTESIAN_POINT ( 'NONE',  ( -4.999999999999999112, -1.831125658499874964, -1.158123955083390388 ) ) ;
#27585=CARTESIAN_POINT ( 'NONE',  ( 0.3476802294499899415, 5.572769417831398897, -1.687189089856316215 ) ) ;
#27789=ORIENTED_EDGE ( 'NONE', *, *, #600, .T. ) ;
#27864=CARTESIAN_POINT ( 'NONE',  ( -3.675296855064184687, 3.651569063273166993, -0.8655517945778067324 ) ) ;
#27885=( NAMED_UNIT ( * ) SI_UNIT ( $, .STERADIAN. ) SOLID_ANGLE_UNIT ( ) );
#27915=PLANE ( 'NONE',  #6025 ) ;
#28014=CARTESIAN_POINT ( 'NONE',  ( -5.000000000000000000, -0.4878135028931876449, -6.000000000000001776 ) ) ;
#28021=ORIENTED_EDGE ( 'NONE', *, *, #1803, .T. ) ;
#28024=VERTEX_POINT ( 'NONE', #1126 ) ;
#28176=EDGE_LOOP ( 'NONE', ( #21075, #30514, #3453 ) ) ;
#28222=ORIENTED_EDGE ( 'NONE', *, *, #10333, .T. ) ;
#28305=EDGE_LOOP ( 'NONE', ( #10107, #6429, #23656 ) ) ;
#28339=PLANE ( 'NONE',  #32541 ) ;
#28368=AXIS2_PLACEMENT_3D ( 'NONE', #34055, #22803, #2924 ) ;
#28372=EDGE_CURVE ( 'NONE', #28959, #16790, #24573, .T. ) ;
#28428=EDGE_CURVE ( 'NONE', #20425, #15155, #5720, .T. ) ;
#28458=CARTESIAN_POINT ( 'NONE',  ( 0.000000000000000000, 5.773502691896262640, -6.000000000000000000 ) ) ;
#28480=EDGE_CURVE ( 'NONE', #24664, #34239, #17672, .T. ) ;
#28509=EDGE_LOOP ( 'NONE', ( #16578, #27789 ) ) ;
#28663=CYLINDRICAL_SURFACE ( 'NONE', #20535, 2.500000000000000000 ) ;
#28824=CARTESIAN_POINT ( 'NONE',  ( 0.000000000000000000, 0.000000000000000000, -6.000000000000000000 ) ) ;
#28935=CARTESIAN_POINT ( 'NONE',  ( 2.991272306860053298, -4.046490820311139380, -0.5592653008974324269 ) ) ;
#28959=VERTEX_POINT ( 'NONE', #6057 ) ;
#29018=CARTESIAN_POINT ( 'NONE',  ( 2.500000000000003109, -4.330127018922192761, -6.000000000000000000 ) ) ;
#29060=DIRECTION ( 'NONE',  ( 1.000000000000000000, 0.000000000000000000, 0.000000000000000000 ) ) ;
#29067=AXIS2_PLACEMENT_3D ( 'NONE', #24261, #13012, #35715 ) ;
#29094=PLANE ( 'NONE',  #5601 ) ;
#29127=CARTESIAN_POINT ( 'NONE',  ( 1.332830945733272987, -5.003992386592898356, -0.8603634151101718919 ) ) ;
#29153=DIRECTION ( 'NONE',  ( -1.000000000000000000, 0.000000000000000000, 0.000000000000000000 ) ) ;
#29220=CARTESIAN_POINT ( 'NONE',  ( 2.074714256722481664, -4.575665857285986959, -5.989444439476606874 ) ) ;
#29235=AXIS2_PLACEMENT_3D ( 'NONE', #7311, #36180, #6935 ) ;
#29409=CARTESIAN_POINT ( 'NONE',  ( 5.000000000000000000, 2.886751345948137981, -5.553418012614792509 ) ) ;
#29452=CARTESIAN_POINT ( 'NONE',  ( 5.000000000000000000, 2.886751345948137981, -5.553418012614792509 ) ) ;
#29488=CARTESIAN_POINT ( 'NONE',  ( 0.7207917504152147048, -5.357353380764381612, -1.325189086772950331 ) ) ;
#29512=CARTESIAN_POINT ( 'NONE',  ( 5.000000000000000000, 1.352381405509861523, -0.8629530094790043293 ) ) ;
#29610=AXIS2_PLACEMENT_3D ( 'NONE', #6380, #27001, #6747 ) ;
#29658=EDGE_LOOP ( 'NONE', ( #13982, #14906, #12728, #18843 ) ) ;
#29728=ORIENTED_EDGE ( 'NONE', *, *, #24949, .T. ) ;
#29736=DIRECTION ( 'NONE',  ( 0.000000000000000000, 0.000000000000000000, 1.000000000000000000 ) ) ;
#29787=VERTEX_POINT ( 'NONE', #15659 ) ;
#29825=EDGE_CURVE ( 'NONE', #34239, #24664, #12990, .T. ) ;
#29884=LINE ( 'NONE', #18073, #5508 ) ;
#29902=DIRECTION ( 'NONE',  ( 0.000000000000000000, 0.000000000000000000, 1.000000000000000000 ) ) ;
#29954=DIRECTION ( 'NONE',  ( 1.000000000000000000, 0.000000000000000000, 0.000000000000000000 ) ) ;
#29976=EDGE_CURVE ( 'NONE', #32183, #29787, #17497, .T. ) ;
#30004=CARTESIAN_POINT ( 'NONE',  ( -5.000000000000000000, 2.488344183252603870, -1.689918788536291405 ) ) ;
#30125=ORIENTED_EDGE ( 'NONE', *, *, #2930, .T. ) ;
#30218=CARTESIAN_POINT ( 'NONE',  ( -4.084562121000262280, -3.415279651815011253, -1.156968425231159614 ) ) ;
#30287=DIRECTION ( 'NONE',  ( 1.000000000000000000, 0.000000000000000000, 0.000000000000000000 ) ) ;
#30306=AXIS2_PLACEMENT_3D ( 'NONE', #8473, #34344, #29060 ) ;
#30316=CARTESIAN_POINT ( 'NONE',  ( 0.000000000000000000, 0.000000000000000000, 0.000000000000000000 ) ) ;
#30335=FILL_AREA_STYLE_COLOUR ( '', #35152 ) ;
#30344=CARTESIAN_POINT ( 'NONE',  ( -2.712167343862821323, -4.207632145829752979, -6.000000000000000888 ) ) ;
#30347=CONICAL_SURFACE ( 'NONE', #22564, 3.000000000000000000, 0.9599310885968762586 ) ;
#30376=DIRECTION ( 'NONE',  ( 0.4415113423096792000, 5.406954521468000113E-17, -0.8972556684757725387 ) ) ;
#30384=DIRECTION ( 'NONE',  ( 0.000000000000000000, 0.000000000000000000, 1.000000000000000000 ) ) ;
#30418=DIRECTION ( 'NONE',  ( -1.000000000000000000, 0.000000000000000000, 0.000000000000000000 ) ) ;
#30469=DIRECTION ( 'NONE',  ( 0.000000000000000000, 0.000000000000000000, -1.000000000000000000 ) ) ;
#30477=ADVANCED_BREP_SHAPE_REPRESENTATION ( '', ( #7743, #21385 ), #33942 ) ;
#30514=ORIENTED_EDGE ( 'NONE', *, *, #29976, .T. ) ;
#30558=EDGE_CURVE ( 'NONE', #21666, #16670, #183, .T. ) ;
#30661=DIRECTION ( 'NONE',  ( 0.000000000000000000, 0.000000000000000000, 1.000000000000000000 ) ) ;
#30681=CARTESIAN_POINT ( 'NONE',  ( -4.829002333675109782, 2.985476894631601485, -1.879366290983708110 ) ) ;
#30737=CARTESIAN_POINT ( 'NONE',  ( 4.999999999999999112, -0.1416384297035287454, -0.5080592402122392492 ) ) ;
#30804=CARTESIAN_POINT ( 'NONE',  ( -5.000000000000000888, -1.936377641173862463, -5.802630826755077464 ) ) ;
#30813=CARTESIAN_POINT ( 'NONE',  ( -3.000000000000000000, 3.673940397442059868E-16, -6.000000000000001776 ) ) ;
#30873=AXIS2_PLACEMENT_3D ( 'NONE', #322, #4449, #9527 ) ;
#30889=CARTESIAN_POINT ( 'NONE',  ( -3.346878500200759277, -3.841181488860386573, -5.948595712916170619 ) ) ;
#30914=ADVANCED_FACE ( 'NONE', ( #4494 ), #34669, .T. ) ;
#30922=CARTESIAN_POINT ( 'NONE',  ( 4.999999999999999112, -2.691295138309024892, -1.881393335304215153 ) ) ;
#30955=CARTESIAN_POINT ( 'NONE',  ( 0.000000000000000000, 0.000000000000000000, -5.974599999999999689 ) ) ;
#30985=B_SPLINE_CURVE_WITH_KNOTS ( 'NONE', 3,
 ( #21099, #27273, #9494, #24106, #9841, #9674 ),
 .UNSPECIFIED., .F., .F.,
 ( 4, 2, 4 ),
 ( 0.008070708573309213693, 0.009531758523483287518, 0.01099280847365736134 ),
 .UNSPECIFIED. ) ;
#31092=CARTESIAN_POINT ( 'NONE',  ( -2.500000000000003997, -4.330127018922192761, -6.000000000000000000 ) ) ;
#31167=ADVANCED_FACE ( 'NONE', ( #5979 ), #36752, .T. ) ;
#31330=CARTESIAN_POINT ( 'NONE',  ( 5.000000000000000888, 0.000000000000000000, -6.000000000000000000 ) ) ;
#31363=CIRCLE ( 'NONE', #10389, 3.000000000000000000 ) ;
#31481=AXIS2_PLACEMENT_3D ( 'NONE', #24836, #15833, #29902 ) ;
#31515=CARTESIAN_POINT ( 'NONE',  ( 4.999999999999999112, -2.417244626924488049, -5.688952927922135139 ) ) ;
#31532=ORIENTED_EDGE ( 'NONE', *, *, #2091, .F. ) ;
#31756=CARTESIAN_POINT ( 'NONE',  ( 2.381231458764692110, -4.398698068175666442, -0.5078976954043025183 ) ) ;
#31758=VECTOR ( 'NONE', #11072, 1000.000000000000000 ) ;
#31760=CARTESIAN_POINT ( 'NONE',  ( 1.301042606982605321E-15, 5.773502691896264416, -5.553418012614792509 ) ) ;
#31765=CYLINDRICAL_SURFACE ( 'NONE', #12553, 2.500000000000000000 ) ;
#31784=CARTESIAN_POINT ( 'NONE',  ( -5.000000000000000000, -4.846777557549235459E-18, -0.5080592402122449114 ) ) ;
#31853=ADVANCED_FACE ( 'NONE', ( #11813 ), #32040, .F. ) ;
#31901=ORIENTED_EDGE ( 'NONE', *, *, #22864, .F. ) ;
#32040=CYLINDRICAL_SURFACE ( 'NONE', #29610, 3.000000000000000000 ) ;
#32047=CARTESIAN_POINT ( 'NONE',  ( 4.182066831946704255, -3.358985280702828646, -5.826062401966622950 ) ) ;
#32114=CARTESIAN_POINT ( 'NONE',  ( 1.552113441248130554, -4.877389578778822177, -0.7348938709837993244 ) ) ;
#32151=AXIS2_PLACEMENT_3D ( 'NONE', #6660, #26908, #29153 ) ;
#32183=VERTEX_POINT ( 'NONE', #2246 ) ;
#32198=B_SPLINE_CURVE_WITH_KNOTS ( 'NONE', 3,
 ( #10825, #30681, #7999, #16635, #10637, #27864, #2562, #36136, #11177, #36690, #7640, #19438, #21876, #1997, #25430, #5001, #22257, #24703, #22081, #16089 ),
 .UNSPECIFIED., .F., .F.,
 ( 4, 2, 2, 2, 2, 2, 2, 2, 2, 4 ),
 ( 2.781148944365360171E-07, 0.0008372784139787578517, 0.001674278713063079033, 0.002511279012147400649, 0.003348279311231721830, 0.003766779460773882204, 0.004185279610316042578, 0.005022279909400362459, 0.005859280208484684074, 0.006696280507569004822 ),
 .UNSPECIFIED. ) ;
#32300=VERTEX_POINT ( 'NONE', #12119 ) ;
#32460=CARTESIAN_POINT ( 'NONE',  ( 0.000000000000000000, 5.773502691896262640, 0.000000000000000000 ) ) ;
#32512=CARTESIAN_POINT ( 'NONE',  ( 4.999999999999999112, 0.2838785441256751474, -0.5080592402122395823 ) ) ;
#32535=DIRECTION ( 'NONE',  ( 0.000000000000000000, 0.000000000000000000, 1.000000000000000000 ) ) ;
#32541=AXIS2_PLACEMENT_3D ( 'NONE', #8846, #5863, #20095 ) ;
#32544=AXIS2_PLACEMENT_3D ( 'NONE', #30955, #21609, #13518 ) ;
#32561=AXIS2_PLACEMENT_3D ( 'NONE', #28824, #23217, #34673 ) ;
#32674=ORIENTED_EDGE ( 'NONE', *, *, #25444, .F. ) ;
#32709=EDGE_CURVE ( 'NONE', #27114, #21666, #24302, .T. ) ;
#32724=B_SPLINE_CURVE_WITH_KNOTS ( 'NONE', 3,
 ( #13794, #25234, #24857, #7799, #16798, #37039, #36294, #10605 ),
 .UNSPECIFIED., .F., .F.,
 ( 4, 2, 2, 4 ),
 ( 0.002921158011986710323, 0.003648658599403066614, 0.004376159186819422904, 0.005831160361652134617 ),
 .UNSPECIFIED. ) ;
#32735=DIRECTION ( 'NONE',  ( -0.000000000000000000, -0.000000000000000000, 1.000000000000000000 ) ) ;
#32744=LINE ( 'NONE', #7625, #17261 ) ;
#32792=CARTESIAN_POINT ( 'NONE',  ( 2.712167343862820434, 4.207632145829745873, -6.000000000000002665 ) ) ;
#32793=DIRECTION ( 'NONE',  ( 0.000000000000000000, 0.000000000000000000, -1.000000000000000000 ) ) ;
#32840=ADVANCED_FACE ( 'NONE', ( #19037 ), #10029, .F. ) ;
#32841=CARTESIAN_POINT ( 'NONE',  ( 4.084562121000262280, 3.415279651815005924, -1.156968425231149844 ) ) ;
#32848=CARTESIAN_POINT ( 'NONE',  ( 0.000000000000000000, 0.000000000000000000, -0.3851141460153411078 ) ) ;
#32864=VERTEX_POINT ( 'NONE', #7583 ) ;
#32870=ORIENTED_EDGE ( 'NONE', *, *, #8541, .T. ) ;
#32971=EDGE_LOOP ( 'NONE', ( #24727, #2530, #6676, #36044, #20880 ) ) ;
#32992=EDGE_LOOP ( 'NONE', ( #20777, #18215, #35865, #33292 ) ) ;
#33063=DIRECTION ( 'NONE',  ( 0.000000000000000000, 0.000000000000000000, 1.000000000000000000 ) ) ;
#33082=VERTEX_POINT ( 'NONE', #23119 ) ;
#33192=CARTESIAN_POINT ( 'NONE',  ( 0.1709976663248966577, 5.674777143212787145, -1.879366290983712107 ) ) ;
#33218=EDGE_CURVE ( 'NONE', #32300, #2420, #36942, .T. ) ;
#33262=ORIENTED_EDGE ( 'NONE', *, *, #4856, .F. ) ;
#33276=DIRECTION ( 'NONE',  ( -1.000000000000000000, 0.000000000000000000, 0.000000000000000000 ) ) ;
#33292=ORIENTED_EDGE ( 'NONE', *, *, #2987, .T. ) ;
#33294=CIRCLE ( 'NONE', #30873, 5.000000000000000888 ) ;
#33323=STYLED_ITEM ( 'NONE', ( #10109 ), #30477 ) ;
#33341=CARTESIAN_POINT ( 'NONE',  ( -3.351853367131006234, 3.838309248099018411, -6.000000000000003553 ) ) ;
#33345=( LENGTH_UNIT ( ) NAMED_UNIT ( * ) SI_UNIT ( .MILLI., .METRE. ) );
#33388=CARTESIAN_POINT ( 'NONE',  ( 5.000000000000000000, -1.472375319565264684, -0.9369361380397587258 ) ) ;
#33430=AXIS2_PLACEMENT_3D ( 'NONE', #1957, #2522, #33276 ) ;
#33478=FACE_OUTER_BOUND ( 'NONE', #24606, .T. ) ;
#33548=( NAMED_UNIT ( * ) SI_UNIT ( $, .STERADIAN. ) SOLID_ANGLE_UNIT ( ) );
#33559=STYLED_ITEM ( 'NONE', ( #18040 ), #7743 ) ;
#33648=CARTESIAN_POINT ( 'NONE',  ( -5.000000000000000000, -2.886751345948137981, -5.553418012614792509 ) ) ;
#33657=EDGE_LOOP ( 'NONE', ( #35079, #14515, #26116, #8608, #7285, #2519, #6809 ) ) ;
#33712=B_SPLINE_CURVE_WITH_KNOTS ( 'NONE', 3,
 ( #34346, #31515, #20280, #25738, #12003, #31330 ),
 .UNSPECIFIED., .F., .F.,
 ( 4, 2, 4 ),
 ( 0.005150343764683553392, 0.006610526168996383109, 0.008070708573309213693 ),
 .UNSPECIFIED. ) ;
#33734=VECTOR ( 'NONE', #11131, 1000.000000000000000 ) ;
#33787=CARTESIAN_POINT ( 'NONE',  ( -4.651285141664999401, -3.088081963278269004, -1.686035282245272215 ) ) ;
#33914=AXIS2_PLACEMENT_3D ( 'NONE', #10230, #30469, #4603 ) ;
#33942=( GEOMETRIC_REPRESENTATION_CONTEXT ( 3 ) GLOBAL_UNCERTAINTY_ASSIGNED_CONTEXT ( ( #4708 ) ) GLOBAL_UNIT_ASSIGNED_CONTEXT ( ( #33345, #24156, #27885 ) ) REPRESENTATION_CONTEXT ( 'NONE', 'WORKASPACE' ) );
#33979=ORIENTED_EDGE ( 'NONE', *, *, #18555, .F. ) ;
#34048=CARTESIAN_POINT ( 'NONE',  ( 5.000000000000000888, -2.886751345948134873, -2.080000000000000071 ) ) ;
#34055=CARTESIAN_POINT ( 'NONE',  ( 0.000000000000000000, 0.000000000000000000, 0.000000000000000000 ) ) ;
#34146=ADVANCED_FACE ( 'NONE', ( #33478 ), #27409, .F. ) ;
#34230=ORIENTED_EDGE ( 'NONE', *, *, #16868, .F. ) ;
#34239=VERTEX_POINT ( 'NONE', #30813 ) ;
#34295=CARTESIAN_POINT ( 'NONE',  ( 5.000000000000002665, -2.886751345948134873, -5.553418012614792509 ) ) ;
#34307=CARTESIAN_POINT ( 'NONE',  ( 0.4079457818577056916, -5.537975084925947478, -5.689399939901065295 ) ) ;
#34344=DIRECTION ( 'NONE',  ( -0.000000000000000000, -0.000000000000000000, 1.000000000000000000 ) ) ;
#34346=CARTESIAN_POINT ( 'NONE',  ( 5.000000000000002665, -2.886751345948134873, -5.553418012614792509 ) ) ;
#34398=EDGE_CURVE ( 'NONE', #24664, #21710, #6788, .T. ) ;
#34420=ORIENTED_EDGE ( 'NONE', *, *, #2539, .F. ) ;
#34432=CARTESIAN_POINT ( 'NONE',  ( -2.503857664561936813E-16, -5.773502691896267081, -6.000000000000000000 ) ) ;
#34487=ADVANCED_FACE ( 'NONE', ( #25943 ), #18990, .T. ) ;
#34565=VECTOR ( 'NONE', #16877, 1000.000000000000000 ) ;
#34590=ORIENTED_EDGE ( 'NONE', *, *, #36866, .F. ) ;
#34669=CONICAL_SURFACE ( 'NONE', #29235, 4.749999999999999112, 0.4572823821333981131 ) ;
#34673=DIRECTION ( 'NONE',  ( 1.000000000000000000, 0.000000000000000000, 0.000000000000000000 ) ) ;
#34755=( NAMED_UNIT ( * ) SI_UNIT ( $, .STERADIAN. ) SOLID_ANGLE_UNIT ( ) );
#34769=DIRECTION ( 'NONE',  ( -1.000000000000000000, 0.000000000000000000, 0.000000000000000000 ) ) ;
#34856=CARTESIAN_POINT ( 'NONE',  ( 2.287832656137188447, -4.452621892014642313, -5.999999999999999112 ) ) ;
#34897=FACE_OUTER_BOUND ( 'NONE', #28176, .T. ) ;
#35079=ORIENTED_EDGE ( 'NONE', *, *, #600, .F. ) ;
#35134=CARTESIAN_POINT ( 'NONE',  ( 0.000000000000000000, 0.000000000000000000, 0.000000000000000000 ) ) ;
#35135=CARTESIAN_POINT ( 'NONE',  ( -0.7178748134487012988, -5.359037475107207626, -1.327869168827489732 ) ) ;
#35149=PLANE ( 'NONE',  #12864 ) ;
#35152=COLOUR_RGB ( '', 0.31764706, 0.68627451, 0.89019608) ;
#35163=FACE_OUTER_BOUND ( 'NONE', #4059, .T. ) ;
#35257=ADVANCED_FACE ( 'NONE', ( #146 ), #28663, .F. ) ;
#35263=VERTEX_POINT ( 'NONE', #34295 ) ;
#35322=CARTESIAN_POINT ( 'NONE',  ( 0.000000000000000000, 0.000000000000000000, -6.000000000000000000 ) ) ;
#35375=CARTESIAN_POINT ( 'NONE',  ( 5.000000000000000000, 2.886751345948134428, -2.080000000000000071 ) ) ;
#35440=SHAPE_REPRESENTATION ( 'torque nut 03_iso_ISO 7042-M6-N', ( #21385 ), #33942 ) ;
#35535=CARTESIAN_POINT ( 'NONE',  ( 5.000000000000000000, 1.101175676120959901, -0.7375066809288793879 ) ) ;
#35632=EDGE_LOOP ( 'NONE', ( #16121, #7964, #307, #31901, #14954, #6903 ) ) ;
#35715=DIRECTION ( 'NONE',  ( -1.000000000000000000, 3.552713678800500929E-15, 0.000000000000000000 ) ) ;
#35797=SURFACE_STYLE_FILL_AREA ( #7660 ) ;
#35821=CARTESIAN_POINT ( 'NONE',  ( -4.999999999999999112, -2.691295138309024448, -1.881393335304213821 ) ) ;
#35865=ORIENTED_EDGE ( 'NONE', *, *, #2539, .T. ) ;
#36044=ORIENTED_EDGE ( 'NONE', *, *, #24949, .F. ) ;
#36136=CARTESIAN_POINT ( 'NONE',  ( -2.991272306860052410, 4.046490820311134939, -0.5592653008974223239 ) ) ;
#36180=DIRECTION ( 'NONE',  ( 0.000000000000000000, 0.000000000000000000, -1.000000000000000000 ) ) ;
#36181=LINE ( 'NONE', #1868, #6606 ) ;
#36227=VECTOR ( 'NONE', #10986, 1000.000000000000000 ) ;
#36291=ORIENTED_EDGE ( 'NONE', *, *, #19520, .F. ) ;
#36294=CARTESIAN_POINT ( 'NONE',  ( -0.4079457818577069683, 5.537975084925943037, -5.689399939901069736 ) ) ;
#36328=FACE_OUTER_BOUND ( 'NONE', #574, .T. ) ;
#36368=CARTESIAN_POINT ( 'NONE',  ( -5.000000000000000000, -2.886751345948134428, -2.080000000000000071 ) ) ;
#36396=DIRECTION ( 'NONE',  ( 1.000000000000000000, 0.000000000000000000, 0.000000000000000000 ) ) ;
#36431=CARTESIAN_POINT ( 'NONE',  ( -3.101151694651716806, -3.983051926191232717, -0.6020238742160465284 ) ) ;
#36440=ORIENTED_EDGE ( 'NONE', *, *, #8002, .F. ) ;
#36553=ORIENTED_EDGE ( 'NONE', *, *, #12974, .T. ) ;
#36690=CARTESIAN_POINT ( 'NONE',  ( -2.381231458764688558, 4.398698068175660225, -0.5078976954042897507 ) ) ;
#36694=PRODUCT ( 'torque nut 03_iso_ISO 7042-M6-N', 'torque nut 03_iso_ISO 7042-M6-N', '', ( #17553 ) ) ;
#36720=VERTEX_POINT ( 'NONE', #18676 ) ;
#36752=CONICAL_SURFACE ( 'NONE', #32561, 5.000000000000000888, 1.047197551196596299 ) ;
#36760=ORIENTED_EDGE ( 'NONE', *, *, #19294, .F. ) ;
#36815=CARTESIAN_POINT ( 'NONE',  ( -5.000000000000000000, -2.886751345948133540, -6.000000000000000000 ) ) ;
#36866=EDGE_CURVE ( 'NONE', #27114, #2420, #15678, .T. ) ;
#36927=UNCERTAINTY_MEASURE_WITH_UNIT (LENGTH_MEASURE( 1.000000000000000082E-05 ), #25929, 'distance_accuracy_value', 'NONE');
#36942=CIRCLE ( 'NONE', #21951, 2.500000000000000000 ) ;
#36965=LINE ( 'NONE', #4737, #31758 ) ;
#36993=EDGE_CURVE ( 'NONE', #32864, #24448, #32724, .T. ) ;
#37039=CARTESIAN_POINT ( 'NONE',  ( -0.8192951148925873284, 5.300482436767278926, -5.801655677627841179 ) ) ;
#37067=AXIS2_PLACEMENT_3D ( 'NONE', #21346, #32793, #7110 ) ;
#37077=ORIENTED_EDGE ( 'NONE', *, *, #36993, .F. ) ;
ENDSEC;
END-ISO-10303-21;
